ISO-10303-21;
HEADER;
FILE_DESCRIPTION (('STEP AP214'),
    '1' );
FILE_NAME ('Front Plate.step',
    '2026-10-07T18:46:32',
    ( '' ),
    ( '' ),
    'SwSTEP 2.0',
    'SolidWorks 2020',
    '' );
FILE_SCHEMA (( 'AUTOMOTIVE_DESIGN' ));
ENDSEC;

DATA;
#5=APPLICATION_CONTEXT ( 'automotive_design' ) ;
#6=AXIS2_PLACEMENT_3D ( 'NONE', #12347, #7346, #8914 ) ;
#20=ORIENTED_EDGE ( 'NONE', *, *, #5140, .T. ) ;
#26=COLOUR_RGB ( '', 0.09019608, 0.27058824, 0.51372549) ;
#27=EDGE_CURVE ( 'NONE', #7925, #9580, #2768, .T. ) ;
#75=CARTESIAN_POINT ( 'NONE',  ( 29.69597781366221767, 58.69165929845684104, 68.50000000000000000 ) ) ;
#152=EDGE_LOOP ( 'NONE', ( #5352, #6747, #14198, #4227 ) ) ;
#157=CYLINDRICAL_SURFACE ( 'NONE', #6869, 0.2500000000000002220 ) ;
#164=CARTESIAN_POINT ( 'NONE',  ( 29.69597781366221767, 58.69165929845684104, 70.50000000000000000 ) ) ;
#200=CIRCLE ( 'NONE', #4864, 1.750000000000001554 ) ;
#204=PRODUCT_DEFINITION_CONTEXT ( 'detailed design', #5, 'design' ) ;
#209=DIRECTION ( 'NONE',  ( -0.000000000000000000, 0.000000000000000000, 1.000000000000000000 ) ) ;
#234=SURFACE_STYLE_USAGE ( .BOTH. , #3717 ) ;
#255=DIRECTION ( 'NONE',  ( 1.000000000000000000, 0.000000000000000000, 0.000000000000000000 ) ) ;
#283=DIRECTION ( 'NONE',  ( -0.000000000000000000, -0.000000000000000000, 1.000000000000000000 ) ) ;
#318=CARTESIAN_POINT ( 'NONE',  ( -31.69597781366222122, 56.94165929845684815, 70.25000000000000000 ) ) ;
#343=DIRECTION ( 'NONE',  ( -0.000000000000000000, 0.000000000000000000, 1.000000000000000000 ) ) ;
#348=DIRECTION ( 'NONE',  ( 0.000000000000000000, 0.000000000000000000, -1.000000000000000000 ) ) ;
#351=FACE_OUTER_BOUND ( 'NONE', #21954, .T. ) ;
#395=DIRECTION ( 'NONE',  ( -1.000000000000000000, 0.000000000000000000, 0.000000000000000000 ) ) ;
#411=LINE ( 'NONE', #17207, #6330 ) ;
#416=VERTEX_POINT ( 'NONE', #18911 ) ;
#453=SURFACE_STYLE_FILL_AREA ( #20843 ) ;
#480=DIRECTION ( 'NONE',  ( 0.000000000000000000, 1.000000000000000000, 0.000000000000000000 ) ) ;
#529=AXIS2_PLACEMENT_3D ( 'NONE', #21492, #7709, #12948 ) ;
#534=AXIS2_PLACEMENT_3D ( 'NONE', #11478, #21575, #19882 ) ;
#548=DIRECTION ( 'NONE',  ( 1.000000000000000000, 0.000000000000000000, 0.000000000000000000 ) ) ;
#588=CYLINDRICAL_SURFACE ( 'NONE', #16421, 4.193574995607837863 ) ;
#603=ADVANCED_FACE ( 'NONE', ( #20097 ), #16254, .T. ) ;
#604=VECTOR ( 'NONE', #10624, 1000.000000000000000 ) ;
#609=EDGE_CURVE ( 'NONE', #7850, #7925, #16310, .T. ) ;
#636=CARTESIAN_POINT ( 'NONE',  ( 29.69597781366221767, 56.94165929845684104, 70.25000000000000000 ) ) ;
#656=ADVANCED_FACE ( 'NONE', ( #8566 ), #2730, .T. ) ;
#677=FACE_OUTER_BOUND ( 'NONE', #10525, .T. ) ;
#710=ORIENTED_EDGE ( 'NONE', *, *, #609, .T. ) ;
#766=DIRECTION ( 'NONE',  ( -0.000000000000000000, -1.000000000000000000, -0.000000000000000000 ) ) ;
#771=CIRCLE ( 'NONE', #9361, 1.750000000000001554 ) ;
#837=DIRECTION ( 'NONE',  ( -1.000000000000000000, 0.000000000000000000, 0.000000000000000000 ) ) ;
#847=VERTEX_POINT ( 'NONE', #1094 ) ;
#857=VERTEX_POINT ( 'NONE', #18322 ) ;
#862=CARTESIAN_POINT ( 'NONE',  ( 29.69597781366221767, 26.24124249474150972, 68.50000000000000000 ) ) ;
#878=EDGE_CURVE ( 'NONE', #1886, #11776, #20372, .T. ) ;
#897=VERTEX_POINT ( 'NONE', #13506 ) ;
#902=ADVANCED_FACE ( 'NONE', ( #18655 ), #6451, .T. ) ;
#911=CARTESIAN_POINT ( 'NONE',  ( -3.985331397971318079, 42.46645089659917716, 70.50000000000000000 ) ) ;
#931=EDGE_LOOP ( 'NONE', ( #3456, #2330, #20937, #8526 ) ) ;
#943=CARTESIAN_POINT ( 'NONE',  ( 6.424398693589429399E-15, 58.69165929845684104, 68.50000000000000000 ) ) ;
#969=DIRECTION ( 'NONE',  ( -0.000000000000000000, -0.000000000000000000, -1.000000000000000000 ) ) ;
#978=DIRECTION ( 'NONE',  ( 1.000000000000000000, 0.000000000000000000, 0.000000000000000000 ) ) ;
#984=DIRECTION ( 'NONE',  ( -0.000000000000000000, 0.000000000000000000, 1.000000000000000000 ) ) ;
#988=AXIS2_PLACEMENT_3D ( 'NONE', #16517, #4339, #20012 ) ;
#1012=FACE_OUTER_BOUND ( 'NONE', #16285, .T. ) ;
#1016=EDGE_CURVE ( 'NONE', #8010, #5585, #5377, .T. ) ;
#1062=DIRECTION ( 'NONE',  ( -1.000000000000000000, -0.000000000000000000, -0.000000000000000000 ) ) ;
#1081=ORIENTED_EDGE ( 'NONE', *, *, #13056, .F. ) ;
#1093=EDGE_CURVE ( 'NONE', #11281, #17520, #16861, .T. ) ;
#1094=CARTESIAN_POINT ( 'NONE',  ( 29.69597781366221767, 58.94165929845684104, 68.75000000000000000 ) ) ;
#1125=AXIS2_PLACEMENT_3D ( 'NONE', #4401, #4634, #6207 ) ;
#1138=EDGE_CURVE ( 'NONE', #8252, #11281, #11139, .T. ) ;
#1169=FACE_OUTER_BOUND ( 'NONE', #18177, .T. ) ;
#1173=EDGE_CURVE ( 'NONE', #9535, #10367, #771, .T. ) ;
#1234=( NAMED_UNIT ( * ) SI_UNIT ( $, .STERADIAN. ) SOLID_ANGLE_UNIT ( ) );
#1237=DIRECTION ( 'NONE',  ( 0.000000000000000000, 0.000000000000000000, 1.000000000000000000 ) ) ;
#1267=EDGE_CURVE ( 'NONE', #14159, #9535, #14472, .T. ) ;
#1311=EDGE_LOOP ( 'NONE', ( #16611, #19884, #4952, #13956 ) ) ;
#1324=ORIENTED_EDGE ( 'NONE', *, *, #3556, .F. ) ;
#1341=DIRECTION ( 'NONE',  ( 1.000000000000000000, 0.000000000000000000, 0.000000000000000000 ) ) ;
#1354=CIRCLE ( 'NONE', #4950, 0.2500000000000002220 ) ;
#1363=EDGE_CURVE ( 'NONE', #15493, #16055, #6509, .T. ) ;
#1366=DIRECTION ( 'NONE',  ( -0.000000000000000000, 0.000000000000000000, 1.000000000000000000 ) ) ;
#1386=EDGE_CURVE ( 'NONE', #8703, #5841, #2450, .T. ) ;
#1437=ORIENTED_EDGE ( 'NONE', *, *, #13979, .T. ) ;
#1460=VERTEX_POINT ( 'NONE', #862 ) ;
#1484=DIRECTION ( 'NONE',  ( 1.000000000000000000, 0.000000000000000000, 0.000000000000000000 ) ) ;
#1499=ORIENTED_EDGE ( 'NONE', *, *, #20702, .T. ) ;
#1501=CARTESIAN_POINT ( 'NONE',  ( 29.69597781366221767, 25.99124249474150972, 68.75000000000000000 ) ) ;
#1540=DIRECTION ( 'NONE',  ( 2.105859220307292343E-16, -1.000000000000000000, 0.000000000000000000 ) ) ;
#1572=ORIENTED_EDGE ( 'NONE', *, *, #1589, .F. ) ;
#1589=EDGE_CURVE ( 'NONE', #5063, #20665, #1680, .T. ) ;
#1646=ADVANCED_FACE ( 'NONE', ( #18771 ), #22031, .T. ) ;
#1648=DIRECTION ( 'NONE',  ( 1.000000000000000000, -0.000000000000000000, 0.000000000000000000 ) ) ;
#1680=CIRCLE ( 'NONE', #16314, 2.000000000000001776 ) ;
#1700=DIRECTION ( 'NONE',  ( 0.000000000000000000, 0.000000000000000000, -1.000000000000000000 ) ) ;
#1704=DIRECTION ( 'NONE',  ( 1.224646799147353207E-16, 1.000000000000000000, 0.000000000000000000 ) ) ;
#1731=ORIENTED_EDGE ( 'NONE', *, *, #21343, .F. ) ;
#1743=AXIS2_PLACEMENT_3D ( 'NONE', #12051, #18902, #3574 ) ;
#1764=CARTESIAN_POINT ( 'NONE',  ( 29.69597781366221767, 56.94165929845684104, 68.75000000000000000 ) ) ;
#1765=CARTESIAN_POINT ( 'NONE',  ( -14.37248138918699425, 42.46645089659917716, 70.50000000000000000 ) ) ;
#1803=CARTESIAN_POINT ( 'NONE',  ( -13.37248138918699425, 42.46645089659917716, 68.50000000000000000 ) ) ;
#1835=VECTOR ( 'NONE', #7797, 1000.000000000000000 ) ;
#1883=CARTESIAN_POINT ( 'NONE',  ( 9.178906393579156386, 42.46645089659917716, 68.50000000000000000 ) ) ;
#1886=VERTEX_POINT ( 'NONE', #4216 ) ;
#1895=EDGE_CURVE ( 'NONE', #847, #9535, #12266, .T. ) ;
#1903=CARTESIAN_POINT ( 'NONE',  ( 31.44597781366222122, 56.94165929845684104, 68.75000000000000000 ) ) ;
#1910=VERTEX_POINT ( 'NONE', #16053 ) ;
#1960=DIRECTION ( 'NONE',  ( 0.000000000000000000, -0.000000000000000000, -1.000000000000000000 ) ) ;
#1985=APPLICATION_CONTEXT ( 'automotive_design' ) ;
#2001=CARTESIAN_POINT ( 'NONE',  ( 0.000000000000000000, 0.000000000000000000, 68.50000000000000000 ) ) ;
#2025=FACE_OUTER_BOUND ( 'NONE', #152, .T. ) ;
#2052=DIRECTION ( 'NONE',  ( -0.000000000000000000, -0.000000000000000000, -1.000000000000000000 ) ) ;
#2072=CYLINDRICAL_SURFACE ( 'NONE', #13846, 4.193574995607837863 ) ;
#2081=CIRCLE ( 'NONE', #14232, 1.750000000000001554 ) ;
#2094=ORIENTED_EDGE ( 'NONE', *, *, #4035, .F. ) ;
#2100=FACE_OUTER_BOUND ( 'NONE', #12467, .T. ) ;
#2122=CARTESIAN_POINT ( 'NONE',  ( -29.69597781366221412, 27.99124249474150972, 70.25000000000000000 ) ) ;
#2141=AXIS2_PLACEMENT_3D ( 'NONE', #5791, #14370, #21222 ) ;
#2170=EDGE_CURVE ( 'NONE', #7987, #416, #8929, .T. ) ;
#2174=ADVANCED_FACE ( 'NONE', ( #10685 ), #588, .F. ) ;
#2229=FACE_BOUND ( 'NONE', #21263, .T. ) ;
#2235=EDGE_LOOP ( 'NONE', ( #710, #15792, #1731, #16469 ) ) ;
#2281=CARTESIAN_POINT ( 'NONE',  ( -29.69597781366221767, 58.94165929845684815, 70.25000000000000000 ) ) ;
#2290=FACE_OUTER_BOUND ( 'NONE', #1311, .T. ) ;
#2308=ORIENTED_EDGE ( 'NONE', *, *, #18668, .F. ) ;
#2311=EDGE_CURVE ( 'NONE', #17419, #5726, #13288, .T. ) ;
#2330=ORIENTED_EDGE ( 'NONE', *, *, #7422, .T. ) ;
#2339=FACE_OUTER_BOUND ( 'NONE', #12760, .T. ) ;
#2389=ORIENTED_EDGE ( 'NONE', *, *, #18129, .F. ) ;
#2433=FACE_OUTER_BOUND ( 'NONE', #11290, .T. ) ;
#2434=DIRECTION ( 'NONE',  ( 1.000000000000000000, 0.000000000000000000, 0.000000000000000000 ) ) ;
#2450=LINE ( 'NONE', #17769, #604 ) ;
#2473=TOROIDAL_SURFACE ( 'NONE', #8206, 1.750000000000000000, 0.2500000000000000000 ) ;
#2494=VECTOR ( 'NONE', #20863, 1000.000000000000000 ) ;
#2542=DIRECTION ( 'NONE',  ( 1.000000000000000000, 0.000000000000000000, 0.000000000000000000 ) ) ;
#2546=AXIS2_PLACEMENT_3D ( 'NONE', #11506, #17068, #6384 ) ;
#2634=AXIS2_PLACEMENT_3D ( 'NONE', #8015, #837, #14816 ) ;
#2651=ORIENTED_EDGE ( 'NONE', *, *, #17785, .F. ) ;
#2705=ORIENTED_EDGE ( 'NONE', *, *, #14543, .F. ) ;
#2723=ORIENTED_EDGE ( 'NONE', *, *, #1173, .F. ) ;
#2730=TOROIDAL_SURFACE ( 'NONE', #6702, 1.750000000000000000, 0.2500000000000000000 ) ;
#2740=DIRECTION ( 'NONE',  ( 0.000000000000000000, 0.000000000000000000, 1.000000000000000000 ) ) ;
#2748=FACE_OUTER_BOUND ( 'NONE', #931, .T. ) ;
#2768=CIRCLE ( 'NONE', #16699, 2.000000000000001776 ) ;
#2775=VECTOR ( 'NONE', #19857, 1000.000000000000000 ) ;
#2784=CARTESIAN_POINT ( 'NONE',  ( -29.69597781366221767, 58.69165929845684815, 68.50000000000000000 ) ) ;
#2814=DIRECTION ( 'NONE',  ( 0.000000000000000000, 1.000000000000000000, 0.000000000000000000 ) ) ;
#2823=DIRECTION ( 'NONE',  ( 1.000000000000000000, 0.000000000000000000, 0.000000000000000000 ) ) ;
#2904=FACE_OUTER_BOUND ( 'NONE', #14726, .T. ) ;
#2937=SURFACE_STYLE_FILL_AREA ( #12980 ) ;
#2964=ORIENTED_EDGE ( 'NONE', *, *, #4035, .T. ) ;
#2990=EDGE_CURVE ( 'NONE', #15493, #416, #8324, .T. ) ;
#2991=EDGE_CURVE ( 'NONE', #8252, #897, #11167, .T. ) ;
#3006=DIRECTION ( 'NONE',  ( 1.000000000000000000, 0.000000000000000000, 0.000000000000000000 ) ) ;
#3028=CARTESIAN_POINT ( 'NONE',  ( -31.69597781366221412, 27.99124249474150972, 70.50000000000000000 ) ) ;
#3038=ORIENTED_EDGE ( 'NONE', *, *, #20316, .F. ) ;
#3041=( NAMED_UNIT ( * ) PLANE_ANGLE_UNIT ( ) SI_UNIT ( $, .RADIAN. ) );
#3046=ORIENTED_EDGE ( 'NONE', *, *, #9096, .F. ) ;
#3062=ADVANCED_FACE ( 'NONE', ( #351 ), #7198, .F. ) ;
#3119=DIRECTION ( 'NONE',  ( -1.000000000000000000, -0.000000000000000000, -0.000000000000000000 ) ) ;
#3139=CIRCLE ( 'NONE', #18496, 4.193574995607837863 ) ;
#3177=FACE_OUTER_BOUND ( 'NONE', #8828, .T. ) ;
#3196=ADVANCED_FACE ( 'NONE', ( #1012 ), #21402, .T. ) ;
#3239=LINE ( 'NONE', #10067, #10308 ) ;
#3280=CARTESIAN_POINT ( 'NONE',  ( 31.69597781366222122, 27.99124249474150972, 70.50000000000000000 ) ) ;
#3314=CARTESIAN_POINT ( 'NONE',  ( 13.37248138918699425, 42.46645089659917716, 68.50000000000000000 ) ) ;
#3315=AXIS2_PLACEMENT_3D ( 'NONE', #21460, #9802, #20105 ) ;
#3317=EDGE_CURVE ( 'NONE', #7284, #14159, #18000, .T. ) ;
#3323=ORIENTED_EDGE ( 'NONE', *, *, #4879, .T. ) ;
#3324=AXIS2_PLACEMENT_3D ( 'NONE', #6880, #13335, #15027 ) ;
#3435=EDGE_LOOP ( 'NONE', ( #5947, #12267, #16933, #6581 ) ) ;
#3447=CIRCLE ( 'NONE', #9159, 0.2500000000000002220 ) ;
#3456=ORIENTED_EDGE ( 'NONE', *, *, #5639, .T. ) ;
#3515=DIRECTION ( 'NONE',  ( -1.000000000000000000, 0.000000000000000000, 0.000000000000000000 ) ) ;
#3556=EDGE_CURVE ( 'NONE', #5726, #5063, #17325, .T. ) ;
#3574=DIRECTION ( 'NONE',  ( 1.000000000000000000, 0.000000000000000000, 0.000000000000000000 ) ) ;
#3622=AXIS2_PLACEMENT_3D ( 'NONE', #14975, #13601, #3006 ) ;
#3646=ADVANCED_FACE ( 'NONE', ( #17772 ), #2473, .T. ) ;
#3655=CIRCLE ( 'NONE', #5806, 5.193574995607838751 ) ;
#3659=DIRECTION ( 'NONE',  ( -0.000000000000000000, -0.000000000000000000, -1.000000000000000000 ) ) ;
#3684=FACE_OUTER_BOUND ( 'NONE', #12824, .T. ) ;
#3717=SURFACE_SIDE_STYLE ('',( #453 ) ) ;
#3784=DIRECTION ( 'NONE',  ( -1.000000000000000000, 0.000000000000000000, 0.000000000000000000 ) ) ;
#3814=ORIENTED_EDGE ( 'NONE', *, *, #11445, .T. ) ;
#3834=CIRCLE ( 'NONE', #16667, 1.750000000000001554 ) ;
#3837=DIRECTION ( 'NONE',  ( 1.000000000000000000, -1.094601647044990554E-16, 0.000000000000000000 ) ) ;
#3871=CIRCLE ( 'NONE', #11360, 4.193574995607837863 ) ;
#3903=ORIENTED_EDGE ( 'NONE', *, *, #2311, .F. ) ;
#3963=ADVANCED_FACE ( 'NONE', ( #2100 ), #5483, .F. ) ;
#3970=CARTESIAN_POINT ( 'NONE',  ( 31.69597781366222122, 56.94165929845684104, 70.50000000000000000 ) ) ;
#4019=DIRECTION ( 'NONE',  ( -0.000000000000000000, -0.000000000000000000, -1.000000000000000000 ) ) ;
#4035=EDGE_CURVE ( 'NONE', #17520, #897, #11384, .T. ) ;
#4039=ORIENTED_EDGE ( 'NONE', *, *, #2990, .T. ) ;
#4042=VERTEX_POINT ( 'NONE', #6251 ) ;
#4048=EDGE_CURVE ( 'NONE', #6536, #8703, #10689, .T. ) ;
#4110=EDGE_LOOP ( 'NONE', ( #3323, #15325, #9629, #15369 ) ) ;
#4132=TOROIDAL_SURFACE ( 'NONE', #10567, 5.193574995607837863, 1.000000000000000000 ) ;
#4216=CARTESIAN_POINT ( 'NONE',  ( -29.69597781366221412, 25.99124249474150972, 70.25000000000000000 ) ) ;
#4227=ORIENTED_EDGE ( 'NONE', *, *, #12070, .F. ) ;
#4243=DIRECTION ( 'NONE',  ( 1.000000000000000000, 0.000000000000000000, 0.000000000000000000 ) ) ;
#4265=ORIENTED_EDGE ( 'NONE', *, *, #11947, .F. ) ;
#4268=CARTESIAN_POINT ( 'NONE',  ( 29.69597781366221767, 56.94165929845684104, 70.50000000000000000 ) ) ;
#4297=CARTESIAN_POINT ( 'NONE',  ( 31.44597781366222122, 56.94165929845684104, 70.50000000000000000 ) ) ;
#4301=CARTESIAN_POINT ( 'NONE',  ( 29.69597781366221767, 27.99124249474150972, 70.50000000000000000 ) ) ;
#4325=VECTOR ( 'NONE', #969, 1000.000000000000000 ) ;
#4339=DIRECTION ( 'NONE',  ( 1.000000000000000000, 2.105859220307292343E-16, -0.000000000000000000 ) ) ;
#4347=DIRECTION ( 'NONE',  ( 1.000000000000000000, 0.000000000000000000, 0.000000000000000000 ) ) ;
#4394=VERTEX_POINT ( 'NONE', #21743 ) ;
#4398=EDGE_CURVE ( 'NONE', #16055, #15493, #10639, .T. ) ;
#4401=CARTESIAN_POINT ( 'NONE',  ( -29.69597781366221412, 27.99124249474150972, 70.50000000000000000 ) ) ;
#4445=CARTESIAN_POINT ( 'NONE',  ( -4.985331397971318523, 42.46645089659917716, 70.50000000000000000 ) ) ;
#4458=CARTESIAN_POINT ( 'NONE',  ( 29.69597781366221767, 58.69165929845684104, 70.25000000000000000 ) ) ;
#4487=DIRECTION ( 'NONE',  ( 1.000000000000000000, 0.000000000000000000, 0.000000000000000000 ) ) ;
#4499=EDGE_LOOP ( 'NONE', ( #10039, #16415, #1081, #17117 ) ) ;
#4519=ORIENTED_EDGE ( 'NONE', *, *, #5723, .F. ) ;
#4533=CARTESIAN_POINT ( 'NONE',  ( 29.69597781366221767, 56.94165929845684104, 68.50000000000000000 ) ) ;
#4541=DIRECTION ( 'NONE',  ( 0.000000000000000000, -0.000000000000000000, 1.000000000000000000 ) ) ;
#4558=LINE ( 'NONE', #9373, #12763 ) ;
#4574=EDGE_LOOP ( 'NONE', ( #11819, #8054, #1437, #13165 ) ) ;
#4577=CARTESIAN_POINT ( 'NONE',  ( 29.69597781366221767, 27.99124249474150972, 70.25000000000000000 ) ) ;
#4619=( NAMED_UNIT ( * ) SI_UNIT ( $, .STERADIAN. ) SOLID_ANGLE_UNIT ( ) );
#4634=DIRECTION ( 'NONE',  ( -0.000000000000000000, 0.000000000000000000, -1.000000000000000000 ) ) ;
#4646=DIRECTION ( 'NONE',  ( -0.000000000000000000, 1.000000000000000000, 0.000000000000000000 ) ) ;
#4665=AXIS2_PLACEMENT_3D ( 'NONE', #10352, #13249, #4980 ) ;
#4686=DIRECTION ( 'NONE',  ( 1.000000000000000000, 0.000000000000000000, 0.000000000000000000 ) ) ;
#4725=AXIS2_PLACEMENT_3D ( 'NONE', #20837, #18936, #548 ) ;
#4731=( NAMED_UNIT ( * ) PLANE_ANGLE_UNIT ( ) SI_UNIT ( $, .RADIAN. ) );
#4761=CARTESIAN_POINT ( 'NONE',  ( 29.69597781366221767, 27.99124249474150972, 70.50000000000000000 ) ) ;
#4764=CARTESIAN_POINT ( 'NONE',  ( 31.44597781366222122, 27.99124249474150972, 68.50000000000000000 ) ) ;
#4800=CARTESIAN_POINT ( 'NONE',  ( 9.178906393579156386, 42.46645089659917716, 69.50000000000000000 ) ) ;
#4826=ORIENTED_EDGE ( 'NONE', *, *, #1093, .T. ) ;
#4832=EDGE_CURVE ( 'NONE', #7436, #16130, #11634, .T. ) ;
#4839=LINE ( 'NONE', #3280, #10663 ) ;
#4864=AXIS2_PLACEMENT_3D ( 'NONE', #4268, #16323, #19704 ) ;
#4879=EDGE_CURVE ( 'NONE', #857, #9580, #8083, .T. ) ;
#4903=CARTESIAN_POINT ( 'NONE',  ( -9.178906393579156386, 42.46645089659917716, 69.50000000000000000 ) ) ;
#4950=AXIS2_PLACEMENT_3D ( 'NONE', #6699, #5015, #11814 ) ;
#4952=ORIENTED_EDGE ( 'NONE', *, *, #10479, .T. ) ;
#4980=DIRECTION ( 'NONE',  ( 0.000000000000000000, 0.000000000000000000, -1.000000000000000000 ) ) ;
#5010=ORIENTED_EDGE ( 'NONE', *, *, #7320, .F. ) ;
#5015=DIRECTION ( 'NONE',  ( 1.000000000000000000, 0.000000000000000000, -0.000000000000000000 ) ) ;
#5023=AXIS2_PLACEMENT_3D ( 'NONE', #18290, #19644, #13008 ) ;
#5027=ORIENTED_EDGE ( 'NONE', *, *, #10518, .F. ) ;
#5063=VERTEX_POINT ( 'NONE', #13990 ) ;
#5077=LINE ( 'NONE', #18713, #13980 ) ;
#5130=VERTEX_POINT ( 'NONE', #12857 ) ;
#5135=ORIENTED_EDGE ( 'NONE', *, *, #13056, .T. ) ;
#5140=EDGE_CURVE ( 'NONE', #15087, #16789, #200, .T. ) ;
#5148=DIRECTION ( 'NONE',  ( 0.000000000000000000, -1.000000000000000000, 0.000000000000000000 ) ) ;
#5257=DIRECTION ( 'NONE',  ( -0.000000000000000000, 0.000000000000000000, 1.000000000000000000 ) ) ;
#5309=DIRECTION ( 'NONE',  ( 0.000000000000000000, 0.000000000000000000, -1.000000000000000000 ) ) ;
#5352=ORIENTED_EDGE ( 'NONE', *, *, #2991, .F. ) ;
#5377=CIRCLE ( 'NONE', #17859, 4.193574995607837863 ) ;
#5386=UNCERTAINTY_MEASURE_WITH_UNIT (LENGTH_MEASURE( 1.000000000000000082E-05 ), #14782, 'distance_accuracy_value', 'NONE');
#5412=CARTESIAN_POINT ( 'NONE',  ( 29.69597781366221767, 56.94165929845684104, 70.50000000000000000 ) ) ;
#5463=VERTEX_POINT ( 'NONE', #14841 ) ;
#5470=ADVANCED_FACE ( 'NONE', ( #13386 ), #5962, .T. ) ;
#5483=PLANE ( 'NONE',  #6056 ) ;
#5516=AXIS2_PLACEMENT_3D ( 'NONE', #18894, #13718, #10159 ) ;
#5585=VERTEX_POINT ( 'NONE', #1803 ) ;
#5604=VECTOR ( 'NONE', #8774, 1000.000000000000000 ) ;
#5630=VECTOR ( 'NONE', #15693, 1000.000000000000000 ) ;
#5633=DIRECTION ( 'NONE',  ( -1.000000000000000000, -2.105859220307275826E-16, 0.000000000000000000 ) ) ;
#5639=EDGE_CURVE ( 'NONE', #1886, #9580, #8291, .T. ) ;
#5658=ORIENTED_EDGE ( 'NONE', *, *, #1386, .F. ) ;
#5666=AXIS2_PLACEMENT_3D ( 'NONE', #636, #10611, #19440 ) ;
#5723=EDGE_CURVE ( 'NONE', #17419, #16789, #19143, .T. ) ;
#5726=VERTEX_POINT ( 'NONE', #17880 ) ;
#5739=ORIENTED_EDGE ( 'NONE', *, *, #11947, .T. ) ;
#5760=ORIENTED_EDGE ( 'NONE', *, *, #12240, .F. ) ;
#5776=AXIS2_PLACEMENT_3D ( 'NONE', #14622, #16286, #21359 ) ;
#5791=CARTESIAN_POINT ( 'NONE',  ( -31.44597781366222122, 56.94165929845684815, 68.75000000000000000 ) ) ;
#5798=ORIENTED_EDGE ( 'NONE', *, *, #4832, .F. ) ;
#5804=AXIS2_PLACEMENT_3D ( 'NONE', #8709, #12038, #15504 ) ;
#5805=ADVANCED_FACE ( 'NONE', ( #2904 ), #11505, .T. ) ;
#5806=AXIS2_PLACEMENT_3D ( 'NONE', #13084, #20259, #1341 ) ;
#5826=DIRECTION ( 'NONE',  ( 1.000000000000000000, 0.000000000000000000, 0.000000000000000000 ) ) ;
#5837=ORIENTED_EDGE ( 'NONE', *, *, #11445, .F. ) ;
#5841=VERTEX_POINT ( 'NONE', #9948 ) ;
#5847=DIRECTION ( 'NONE',  ( -0.000000000000000000, 0.000000000000000000, 1.000000000000000000 ) ) ;
#5865=ADVANCED_FACE ( 'NONE', ( #13292 ), #18552, .T. ) ;
#5941=ORIENTED_EDGE ( 'NONE', *, *, #21708, .T. ) ;
#5946=EDGE_CURVE ( 'NONE', #1910, #7925, #8374, .T. ) ;
#5947=ORIENTED_EDGE ( 'NONE', *, *, #13979, .F. ) ;
#5956=DIRECTION ( 'NONE',  ( 1.000000000000000000, -1.094601647044990554E-16, 0.000000000000000000 ) ) ;
#5962=TOROIDAL_SURFACE ( 'NONE', #9882, 1.750000000000000000, 0.2500000000000000000 ) ;
#5993=DIRECTION ( 'NONE',  ( -0.000000000000000000, 0.000000000000000000, 1.000000000000000000 ) ) ;
#6038=LINE ( 'NONE', #4445, #4325 ) ;
#6056=AXIS2_PLACEMENT_3D ( 'NONE', #17209, #3784, #9046 ) ;
#6093=ADVANCED_FACE ( 'NONE', ( #17855 ), #11607, .T. ) ;
#6106=ORIENTED_EDGE ( 'NONE', *, *, #10518, .T. ) ;
#6153=CARTESIAN_POINT ( 'NONE',  ( 29.69597781366221767, 27.99124249474150972, 68.75000000000000000 ) ) ;
#6173=DIRECTION ( 'NONE',  ( -0.000000000000000000, 0.000000000000000000, 1.000000000000000000 ) ) ;
#6185=CARTESIAN_POINT ( 'NONE',  ( -3.985331397971318079, 42.46645089659917716, 69.50000000000000000 ) ) ;
#6199=( LENGTH_UNIT ( ) NAMED_UNIT ( * ) SI_UNIT ( .MILLI., .METRE. ) );
#6207=DIRECTION ( 'NONE',  ( -1.000000000000000000, 0.000000000000000000, 0.000000000000000000 ) ) ;
#6222=( GEOMETRIC_REPRESENTATION_CONTEXT ( 3 ) GLOBAL_UNCERTAINTY_ASSIGNED_CONTEXT ( ( #5386 ) ) GLOBAL_UNIT_ASSIGNED_CONTEXT ( ( #14782, #4731, #4619 ) ) REPRESENTATION_CONTEXT ( 'NONE', 'WORKASPACE' ) );
#6236=CYLINDRICAL_SURFACE ( 'NONE', #3315, 4.193574995607837863 ) ;
#6251=CARTESIAN_POINT ( 'NONE',  ( 31.69597781366222122, 56.94165929845684104, 68.75000000000000000 ) ) ;
#6302=AXIS2_PLACEMENT_3D ( 'NONE', #12194, #343, #20840 ) ;
#6326=CARTESIAN_POINT ( 'NONE',  ( 31.69597781366222122, 58.94165929845684104, 68.75000000000000000 ) ) ;
#6330=VECTOR ( 'NONE', #9042, 1000.000000000000000 ) ;
#6364=EDGE_LOOP ( 'NONE', ( #9376, #10754, #7384, #12131 ) ) ;
#6376=AXIS2_PLACEMENT_3D ( 'NONE', #13345, #13577, #3515 ) ;
#6384=DIRECTION ( 'NONE',  ( 0.000000000000000000, 0.000000000000000000, -1.000000000000000000 ) ) ;
#6427=DIRECTION ( 'NONE',  ( -1.000000000000000000, 1.094601647044990554E-16, 0.000000000000000000 ) ) ;
#6451=TOROIDAL_SURFACE ( 'NONE', #18946, 1.750000000000000000, 0.2500000000000000000 ) ;
#6465=ORIENTED_EDGE ( 'NONE', *, *, #6524, .T. ) ;
#6509=CIRCLE ( 'NONE', #19007, 5.193574995607837863 ) ;
#6523=AXIS2_PLACEMENT_3D ( 'NONE', #7030, #1960, #15611 ) ;
#6524=EDGE_CURVE ( 'NONE', #15631, #15087, #21311, .T. ) ;
#6536=VERTEX_POINT ( 'NONE', #17936 ) ;
#6544=AXIS2_PLACEMENT_3D ( 'NONE', #2001, #209, #14190 ) ;
#6566=DIRECTION ( 'NONE',  ( -1.000000000000000000, 0.000000000000000000, 0.000000000000000000 ) ) ;
#6569=ORIENTED_EDGE ( 'NONE', *, *, #878, .F. ) ;
#6581=ORIENTED_EDGE ( 'NONE', *, *, #878, .T. ) ;
#6591=DIRECTION ( 'NONE',  ( -2.105859220307292343E-16, 1.000000000000000000, -0.000000000000000000 ) ) ;
#6615=CARTESIAN_POINT ( 'NONE',  ( -29.69597781366221412, 25.99124249474150972, 70.50000000000000000 ) ) ;
#6668=ADVANCED_FACE ( 'NONE', ( #3177 ), #11949, .T. ) ;
#6699=CARTESIAN_POINT ( 'NONE',  ( 29.69597781366221767, 26.24124249474150972, 70.25000000000000000 ) ) ;
#6702=AXIS2_PLACEMENT_3D ( 'NONE', #13470, #15575, #255 ) ;
#6714=DIRECTION ( 'NONE',  ( 2.105859220307292343E-16, -1.000000000000000000, 0.000000000000000000 ) ) ;
#6716=LINE ( 'NONE', #18776, #14489 ) ;
#6747=ORIENTED_EDGE ( 'NONE', *, *, #19216, .F. ) ;
#6758=TOROIDAL_SURFACE ( 'NONE', #12784, 1.750000000000000000, 0.2500000000000000000 ) ;
#6766=ORIENTED_EDGE ( 'NONE', *, *, #20434, .T. ) ;
#6829=CIRCLE ( 'NONE', #5023, 4.193574995607837863 ) ;
#6839=LINE ( 'NONE', #20579, #21028 ) ;
#6848=DIRECTION ( 'NONE',  ( 0.000000000000000000, 0.000000000000000000, -1.000000000000000000 ) ) ;
#6869=AXIS2_PLACEMENT_3D ( 'NONE', #8787, #17385, #12331 ) ;
#6880=CARTESIAN_POINT ( 'NONE',  ( -31.44597781366222122, 56.94165929845684815, 70.25000000000000000 ) ) ;
#6926=LINE ( 'NONE', #15500, #7915 ) ;
#6931=FACE_OUTER_BOUND ( 'NONE', #8900, .T. ) ;
#6934=DIRECTION ( 'NONE',  ( 1.000000000000000000, 0.000000000000000000, 0.000000000000000000 ) ) ;
#6949=ORIENTED_EDGE ( 'NONE', *, *, #12466, .T. ) ;
#7017=DIRECTION ( 'NONE',  ( 1.000000000000000000, 0.000000000000000000, 0.000000000000000000 ) ) ;
#7030=CARTESIAN_POINT ( 'NONE',  ( -29.69597781366221767, 56.94165929845684815, 70.25000000000000000 ) ) ;
#7057=CARTESIAN_POINT ( 'NONE',  ( 31.44597781366222122, 56.94165929845684104, 70.25000000000000000 ) ) ;
#7108=CIRCLE ( 'NONE', #19978, 2.000000000000001776 ) ;
#7114=EDGE_LOOP ( 'NONE', ( #21491, #21111, #1499, #17628 ) ) ;
#7163=CIRCLE ( 'NONE', #6, 0.2500000000000002220 ) ;
#7198=PLANE ( 'NONE',  #18682 ) ;
#7235=EDGE_LOOP ( 'NONE', ( #21059, #10505, #4265, #14041 ) ) ;
#7241=CARTESIAN_POINT ( 'NONE',  ( -9.178906393579156386, 42.46645089659917716, 70.50000000000000000 ) ) ;
#7283=DIRECTION ( 'NONE',  ( 1.000000000000000000, 0.000000000000000000, 0.000000000000000000 ) ) ;
#7284=VERTEX_POINT ( 'NONE', #16167 ) ;
#7320=EDGE_CURVE ( 'NONE', #8703, #1886, #17327, .T. ) ;
#7346=DIRECTION ( 'NONE',  ( 1.000000000000000000, 0.000000000000000000, 0.000000000000000000 ) ) ;
#7370=LINE ( 'NONE', #14170, #17429 ) ;
#7384=ORIENTED_EDGE ( 'NONE', *, *, #12466, .F. ) ;
#7402=CIRCLE ( 'NONE', #19914, 1.750000000000001554 ) ;
#7422=EDGE_CURVE ( 'NONE', #9580, #18991, #8583, .T. ) ;
#7436=VERTEX_POINT ( 'NONE', #3314 ) ;
#7461=SHAPE_REPRESENTATION ( 'Front Plate', ( #17493 ), #6222 ) ;
#7462=CARTESIAN_POINT ( 'NONE',  ( 31.44597781366222122, 56.94165929845684104, 68.50000000000000000 ) ) ;
#7473=DIRECTION ( 'NONE',  ( 1.000000000000000000, 0.000000000000000000, 0.000000000000000000 ) ) ;
#7495=ORIENTED_EDGE ( 'NONE', *, *, #10782, .F. ) ;
#7545=MECHANICAL_DESIGN_GEOMETRIC_PRESENTATION_REPRESENTATION('',(#18599),#15023);
#7635=CARTESIAN_POINT ( 'NONE',  ( 6.424398693589429399E-15, 58.69165929845684104, 70.25000000000000000 ) ) ;
#7709=DIRECTION ( 'NONE',  ( 0.000000000000000000, 0.000000000000000000, -1.000000000000000000 ) ) ;
#7764=AXIS2_PLACEMENT_3D ( 'NONE', #12134, #18753, #7017 ) ;
#7797=DIRECTION ( 'NONE',  ( 1.000000000000000000, -1.094601647044990554E-16, 0.000000000000000000 ) ) ;
#7804=ADVANCED_FACE ( 'NONE', ( #677 ), #18056, .T. ) ;
#7850=VERTEX_POINT ( 'NONE', #20729 ) ;
#7863=DIRECTION ( 'NONE',  ( 1.094601647044983281E-16, 1.000000000000000000, 0.000000000000000000 ) ) ;
#7868=CARTESIAN_POINT ( 'NONE',  ( -29.69597781366221412, 27.99124249474150972, 68.50000000000000000 ) ) ;
#7914=CARTESIAN_POINT ( 'NONE',  ( -29.69597781366221412, 26.24124249474150972, 70.50000000000000000 ) ) ;
#7915=VECTOR ( 'NONE', #6591, 1000.000000000000000 ) ;
#7917=PLANE ( 'NONE',  #19750 ) ;
#7925=VERTEX_POINT ( 'NONE', #9409 ) ;
#7982=ORIENTED_EDGE ( 'NONE', *, *, #21540, .T. ) ;
#7987=VERTEX_POINT ( 'NONE', #14533 ) ;
#7997=ORIENTED_EDGE ( 'NONE', *, *, #21419, .T. ) ;
#8010=VERTEX_POINT ( 'NONE', #19812 ) ;
#8015=CARTESIAN_POINT ( 'NONE',  ( 29.69597781366221767, 58.69165929845684104, 68.75000000000000000 ) ) ;
#8016=DIRECTION ( 'NONE',  ( 0.000000000000000000, 1.000000000000000000, 0.000000000000000000 ) ) ;
#8025=ORIENTED_EDGE ( 'NONE', *, *, #7422, .F. ) ;
#8030=CARTESIAN_POINT ( 'NONE',  ( -29.69597781366221412, 27.99124249474150972, 70.50000000000000000 ) ) ;
#8043=DIRECTION ( 'NONE',  ( -0.000000000000000000, 0.000000000000000000, 1.000000000000000000 ) ) ;
#8054=ORIENTED_EDGE ( 'NONE', *, *, #5946, .T. ) ;
#8083=CIRCLE ( 'NONE', #16276, 0.2500000000000002220 ) ;
#8131=DIRECTION ( 'NONE',  ( 0.000000000000000000, 0.000000000000000000, -1.000000000000000000 ) ) ;
#8154=DIRECTION ( 'NONE',  ( 1.000000000000000000, 0.000000000000000000, 0.000000000000000000 ) ) ;
#8193=DIRECTION ( 'NONE',  ( 1.000000000000000000, 0.000000000000000000, 0.000000000000000000 ) ) ;
#8206=AXIS2_PLACEMENT_3D ( 'NONE', #4577, #984, #12950 ) ;
#8252=VERTEX_POINT ( 'NONE', #318 ) ;
#8271=CARTESIAN_POINT ( 'NONE',  ( -31.69597781366221412, 26.24124249474150972, 68.75000000000000000 ) ) ;
#8277=AXIS2_PLACEMENT_3D ( 'NONE', #9451, #21777, #14706 ) ;
#8291=LINE ( 'NONE', #6615, #8775 ) ;
#8306=ORIENTED_EDGE ( 'NONE', *, *, #14344, .F. ) ;
#8324=CIRCLE ( 'NONE', #19390, 1.000000000000000888 ) ;
#8351=EDGE_LOOP ( 'NONE', ( #17824, #16339, #6766, #5798 ) ) ;
#8365=EDGE_CURVE ( 'NONE', #416, #7987, #3871, .T. ) ;
#8366=DIRECTION ( 'NONE',  ( 1.000000000000000000, 0.000000000000000000, 0.000000000000000000 ) ) ;
#8374=LINE ( 'NONE', #15185, #9479 ) ;
#8419=ADVANCED_FACE ( 'NONE', ( #14508 ), #19791, .T. ) ;
#8425=EDGE_CURVE ( 'NONE', #15658, #1460, #2081, .T. ) ;
#8480=CIRCLE ( 'NONE', #17389, 1.000000000000000000 ) ;
#8483=DIRECTION ( 'NONE',  ( 1.000000000000000000, 0.000000000000000000, 0.000000000000000000 ) ) ;
#8526=ORIENTED_EDGE ( 'NONE', *, *, #9096, .T. ) ;
#8539=CIRCLE ( 'NONE', #16730, 0.2500000000000002220 ) ;
#8566=FACE_OUTER_BOUND ( 'NONE', #18567, .T. ) ;
#8583=LINE ( 'NONE', #10137, #15896 ) ;
#8622=AXIS2_PLACEMENT_3D ( 'NONE', #5412, #348, #9082 ) ;
#8626=EDGE_LOOP ( 'NONE', ( #18958, #1572, #2705, #5837 ) ) ;
#8636=FACE_BOUND ( 'NONE', #15613, .T. ) ;
#8654=ADVANCED_FACE ( 'NONE', ( #8713 ), #6758, .T. ) ;
#8667=ORIENTED_EDGE ( 'NONE', *, *, #15976, .T. ) ;
#8703=VERTEX_POINT ( 'NONE', #7914 ) ;
#8709=CARTESIAN_POINT ( 'NONE',  ( -29.69597781366221767, 58.69165929845684815, 70.25000000000000000 ) ) ;
#8713=FACE_OUTER_BOUND ( 'NONE', #4499, .T. ) ;
#8734=UNCERTAINTY_MEASURE_WITH_UNIT (LENGTH_MEASURE( 1.000000000000000082E-05 ), #6199, 'distance_accuracy_value', 'NONE');
#8745=DIRECTION ( 'NONE',  ( -0.000000000000000000, 1.000000000000000000, 0.000000000000000000 ) ) ;
#8774=DIRECTION ( 'NONE',  ( -0.000000000000000000, -0.000000000000000000, 1.000000000000000000 ) ) ;
#8775=VECTOR ( 'NONE', #15171, 1000.000000000000000 ) ;
#8787=CARTESIAN_POINT ( 'NONE',  ( 31.44597781366222122, 0.000000000000000000, 70.25000000000000000 ) ) ;
#8828=EDGE_LOOP ( 'NONE', ( #8941, #9984, #19084, #16944 ) ) ;
#8862=AXIS2_PLACEMENT_3D ( 'NONE', #1883, #20530, #10169 ) ;
#8879=ORIENTED_EDGE ( 'NONE', *, *, #13893, .T. ) ;
#8890=LINE ( 'NONE', #3970, #5604 ) ;
#8900=EDGE_LOOP ( 'NONE', ( #10775, #4039, #15802, #14089 ) ) ;
#8914=DIRECTION ( 'NONE',  ( 0.000000000000000000, 0.000000000000000000, -1.000000000000000000 ) ) ;
#8929=CIRCLE ( 'NONE', #17489, 4.193574995607837863 ) ;
#8941=ORIENTED_EDGE ( 'NONE', *, *, #13893, .F. ) ;
#8977=( NAMED_UNIT ( * ) PLANE_ANGLE_UNIT ( ) SI_UNIT ( $, .RADIAN. ) );
#9006=DIRECTION ( 'NONE',  ( -0.000000000000000000, 0.000000000000000000, 1.000000000000000000 ) ) ;
#9030=CARTESIAN_POINT ( 'NONE',  ( 31.44597781366222122, 27.99124249474150972, 70.50000000000000000 ) ) ;
#9042=DIRECTION ( 'NONE',  ( -0.000000000000000000, -1.000000000000000000, -0.000000000000000000 ) ) ;
#9046=DIRECTION ( 'NONE',  ( 0.000000000000000000, 0.000000000000000000, 1.000000000000000000 ) ) ;
#9060=FACE_BOUND ( 'NONE', #20992, .T. ) ;
#9082=DIRECTION ( 'NONE',  ( -1.000000000000000000, 0.000000000000000000, 0.000000000000000000 ) ) ;
#9088=ORIENTED_EDGE ( 'NONE', *, *, #12070, .T. ) ;
#9096=EDGE_CURVE ( 'NONE', #20665, #1886, #14768, .T. ) ;
#9103=DIRECTION ( 'NONE',  ( -1.000000000000000000, 0.000000000000000000, -0.000000000000000000 ) ) ;
#9153=ORIENTED_EDGE ( 'NONE', *, *, #22146, .T. ) ;
#9159=AXIS2_PLACEMENT_3D ( 'NONE', #17948, #4646, #9788 ) ;
#9326=CIRCLE ( 'NONE', #2546, 1.000000000000000888 ) ;
#9338=DIRECTION ( 'NONE',  ( 0.000000000000000000, 1.000000000000000000, 0.000000000000000000 ) ) ;
#9361=AXIS2_PLACEMENT_3D ( 'NONE', #4533, #16392, #7473 ) ;
#9373=CARTESIAN_POINT ( 'NONE',  ( 29.69597781366221767, 58.94165929845684104, 70.25000000000000000 ) ) ;
#9376=ORIENTED_EDGE ( 'NONE', *, *, #11946, .F. ) ;
#9409=CARTESIAN_POINT ( 'NONE',  ( -31.69597781366221412, 27.99124249474150972, 68.75000000000000000 ) ) ;
#9412=DIRECTION ( 'NONE',  ( 0.000000000000000000, -1.000000000000000000, 0.000000000000000000 ) ) ;
#9439=ORIENTED_EDGE ( 'NONE', *, *, #4832, .T. ) ;
#9451=CARTESIAN_POINT ( 'NONE',  ( -29.69597781366221767, 56.94165929845684815, 68.75000000000000000 ) ) ;
#9472=FACE_OUTER_BOUND ( 'NONE', #4574, .T. ) ;
#9479=VECTOR ( 'NONE', #6714, 1000.000000000000000 ) ;
#9486=CARTESIAN_POINT ( 'NONE',  ( 29.69597781366221767, 27.99124249474150972, 68.50000000000000000 ) ) ;
#9506=ORIENTED_EDGE ( 'NONE', *, *, #10479, .F. ) ;
#9535=VERTEX_POINT ( 'NONE', #75 ) ;
#9580=VERTEX_POINT ( 'NONE', #9816 ) ;
#9629=ORIENTED_EDGE ( 'NONE', *, *, #609, .F. ) ;
#9656=DIRECTION ( 'NONE',  ( 0.000000000000000000, -0.000000000000000000, -1.000000000000000000 ) ) ;
#9683=ORIENTED_EDGE ( 'NONE', *, *, #21370, .T. ) ;
#9685=AXIS2_PLACEMENT_3D ( 'NONE', #17671, #5847, #12115 ) ;
#9689=LINE ( 'NONE', #21557, #2775 ) ;
#9745=CARTESIAN_POINT ( 'NONE',  ( 3.985331397971318079, 42.46645089659917716, 69.50000000000000000 ) ) ;
#9764=SURFACE_SIDE_STYLE ('',( #2937 ) ) ;
#9767=CARTESIAN_POINT ( 'NONE',  ( 0.000000000000000000, 0.000000000000000000, 0.000000000000000000 ) ) ;
#9778=STYLED_ITEM ( 'NONE', ( #16564 ), #20354 ) ;
#9788=DIRECTION ( 'NONE',  ( 0.000000000000000000, 0.000000000000000000, 1.000000000000000000 ) ) ;
#9802=DIRECTION ( 'NONE',  ( -0.000000000000000000, -0.000000000000000000, -1.000000000000000000 ) ) ;
#9816=CARTESIAN_POINT ( 'NONE',  ( -29.69597781366221412, 25.99124249474150972, 68.75000000000000000 ) ) ;
#9830=PRODUCT_DEFINITION_SHAPE ( 'NONE', 'NONE',  #15053 ) ;
#9848=AXIS2_PLACEMENT_3D ( 'NONE', #4458, #21257, #14848 ) ;
#9863=EDGE_CURVE ( 'NONE', #17549, #4042, #21656, .T. ) ;
#9871=LINE ( 'NONE', #16680, #16427 ) ;
#9881=FACE_OUTER_BOUND ( 'NONE', #7114, .T. ) ;
#9882=AXIS2_PLACEMENT_3D ( 'NONE', #6153, #20125, #8154 ) ;
#9910=CARTESIAN_POINT ( 'NONE',  ( 29.69597781366221767, 58.94165929845684104, 70.50000000000000000 ) ) ;
#9933=CIRCLE ( 'NONE', #14911, 0.2500000000000002220 ) ;
#9940=DIRECTION ( 'NONE',  ( 1.000000000000000000, 0.000000000000000000, 0.000000000000000000 ) ) ;
#9948=CARTESIAN_POINT ( 'NONE',  ( 29.69597781366221767, 26.24124249474150972, 70.50000000000000000 ) ) ;
#9981=ORIENTED_EDGE ( 'NONE', *, *, #16309, .T. ) ;
#9984=ORIENTED_EDGE ( 'NONE', *, *, #18129, .T. ) ;
#10016=VECTOR ( 'NONE', #20075, 1000.000000000000000 ) ;
#10039=ORIENTED_EDGE ( 'NONE', *, *, #21343, .T. ) ;
#10058=DIRECTION ( 'NONE',  ( 0.000000000000000000, -0.000000000000000000, -1.000000000000000000 ) ) ;
#10067=CARTESIAN_POINT ( 'NONE',  ( -31.44597781366221412, 27.99124249474150972, 70.50000000000000000 ) ) ;
#10137=CARTESIAN_POINT ( 'NONE',  ( -31.69597781366221412, 25.99124249474150972, 68.75000000000000000 ) ) ;
#10159=DIRECTION ( 'NONE',  ( 0.000000000000000000, 0.000000000000000000, 1.000000000000000000 ) ) ;
#10166=ORIENTED_EDGE ( 'NONE', *, *, #20316, .T. ) ;
#10169=DIRECTION ( 'NONE',  ( -1.000000000000000000, 0.000000000000000000, 0.000000000000000000 ) ) ;
#10192=ORIENTED_EDGE ( 'NONE', *, *, #4398, .T. ) ;
#10247=ORIENTED_EDGE ( 'NONE', *, *, #21088, .T. ) ;
#10273=DIRECTION ( 'NONE',  ( 0.000000000000000000, -0.000000000000000000, -1.000000000000000000 ) ) ;
#10308=VECTOR ( 'NONE', #1540, 1000.000000000000000 ) ;
#10310=DIRECTION ( 'NONE',  ( 0.000000000000000000, -0.000000000000000000, -1.000000000000000000 ) ) ;
#10328=VECTOR ( 'NONE', #9338, 1000.000000000000000 ) ;
#10352=CARTESIAN_POINT ( 'NONE',  ( -31.44597781366221412, 27.99124249474150972, 70.25000000000000000 ) ) ;
#10361=ADVANCED_FACE ( 'NONE', ( #2290 ), #2072, .F. ) ;
#10367=VERTEX_POINT ( 'NONE', #7462 ) ;
#10479=EDGE_CURVE ( 'NONE', #416, #5585, #9689, .T. ) ;
#10505=ORIENTED_EDGE ( 'NONE', *, *, #12215, .T. ) ;
#10518=EDGE_CURVE ( 'NONE', #17549, #15658, #3447, .T. ) ;
#10525=EDGE_LOOP ( 'NONE', ( #2389, #8306, #11925, #11177 ) ) ;
#10538=PRESENTATION_STYLE_ASSIGNMENT (( #234 ) ) ;
#10567=AXIS2_PLACEMENT_3D ( 'NONE', #4903, #13714, #8483 ) ;
#10611=DIRECTION ( 'NONE',  ( -0.000000000000000000, 0.000000000000000000, 1.000000000000000000 ) ) ;
#10615=AXIS2_PLACEMENT_3D ( 'NONE', #4761, #11563, #6566 ) ;
#10624=DIRECTION ( 'NONE',  ( 1.000000000000000000, -0.000000000000000000, 0.000000000000000000 ) ) ;
#10639=CIRCLE ( 'NONE', #12750, 5.193574995607837863 ) ;
#10663=VECTOR ( 'NONE', #1700, 1000.000000000000000 ) ;
#10685=FACE_OUTER_BOUND ( 'NONE', #7235, .T. ) ;
#10689=CIRCLE ( 'NONE', #13542, 1.750000000000001554 ) ;
#10754=ORIENTED_EDGE ( 'NONE', *, *, #17869, .T. ) ;
#10775=ORIENTED_EDGE ( 'NONE', *, *, #1363, .F. ) ;
#10779=ORIENTED_EDGE ( 'NONE', *, *, #5723, .T. ) ;
#10782=EDGE_CURVE ( 'NONE', #1460, #857, #6716, .T. ) ;
#10901=ORIENTED_EDGE ( 'NONE', *, *, #21271, .F. ) ;
#10910=EDGE_CURVE ( 'NONE', #10367, #15658, #411, .T. ) ;
#10976=CARTESIAN_POINT ( 'NONE',  ( -31.44597781366220701, -6.622080232047910987E-15, 70.25000000000000000 ) ) ;
#11008=CARTESIAN_POINT ( 'NONE',  ( 31.44597781366222122, 27.99124249474150972, 70.25000000000000000 ) ) ;
#11110=CIRCLE ( 'NONE', #8277, 2.000000000000001776 ) ;
#11114=ORIENTED_EDGE ( 'NONE', *, *, #1895, .F. ) ;
#11139=CIRCLE ( 'NONE', #6523, 2.000000000000001776 ) ;
#11160=CIRCLE ( 'NONE', #20778, 0.2500000000000002220 ) ;
#11167=CIRCLE ( 'NONE', #3324, 0.2500000000000002220 ) ;
#11176=CARTESIAN_POINT ( 'NONE',  ( 29.69597781366221767, 27.99124249474150972, 68.75000000000000000 ) ) ;
#11177=ORIENTED_EDGE ( 'NONE', *, *, #11970, .F. ) ;
#11207=PRODUCT_DEFINITION_FORMATION_WITH_SPECIFIED_SOURCE ( 'ANY', '', #15181, .NOT_KNOWN. ) ;
#11266=CARTESIAN_POINT ( 'NONE',  ( -9.178906393579156386, 42.46645089659917716, 69.50000000000000000 ) ) ;
#11281=VERTEX_POINT ( 'NONE', #2281 ) ;
#11290=EDGE_LOOP ( 'NONE', ( #3814, #6465, #20, #10166, #2964, #9088, #12897, #11658 ) ) ;
#11360=AXIS2_PLACEMENT_3D ( 'NONE', #11266, #8043, #4243 ) ;
#11364=DIRECTION ( 'NONE',  ( -0.000000000000000000, 0.000000000000000000, 1.000000000000000000 ) ) ;
#11384=CIRCLE ( 'NONE', #1743, 1.750000000000001554 ) ;
#11390=DIRECTION ( 'NONE',  ( 0.000000000000000000, -1.000000000000000000, 0.000000000000000000 ) ) ;
#11445=EDGE_CURVE ( 'NONE', #5841, #15631, #3834, .T. ) ;
#11478=CARTESIAN_POINT ( 'NONE',  ( -29.69597781366221412, 26.24124249474150972, 70.25000000000000000 ) ) ;
#11481=ORIENTED_EDGE ( 'NONE', *, *, #1138, .T. ) ;
#11486=CIRCLE ( 'NONE', #3622, 5.193574995607838751 ) ;
#11505=CYLINDRICAL_SURFACE ( 'NONE', #529, 2.000000000000001776 ) ;
#11506=CARTESIAN_POINT ( 'NONE',  ( 14.37248138918699425, 42.46645089659917716, 69.50000000000000000 ) ) ;
#11534=SURFACE_STYLE_USAGE ( .BOTH. , #9764 ) ;
#11563=DIRECTION ( 'NONE',  ( 0.000000000000000000, 0.000000000000000000, -1.000000000000000000 ) ) ;
#11579=VERTEX_POINT ( 'NONE', #13424 ) ;
#11607=TOROIDAL_SURFACE ( 'NONE', #14460, 1.750000000000000000, 0.2500000000000000000 ) ;
#11627=DIRECTION ( 'NONE',  ( 1.000000000000000000, 0.000000000000000000, 0.000000000000000000 ) ) ;
#11634=CIRCLE ( 'NONE', #17010, 4.193574995607837863 ) ;
#11644=ORIENTED_EDGE ( 'NONE', *, *, #7320, .T. ) ;
#11655=DIRECTION ( 'NONE',  ( -0.000000000000000000, 0.000000000000000000, 1.000000000000000000 ) ) ;
#11658=ORIENTED_EDGE ( 'NONE', *, *, #1386, .T. ) ;
#11661=FACE_OUTER_BOUND ( 'NONE', #8351, .T. ) ;
#11705=ADVANCED_FACE ( 'NONE', ( #2339 ), #22081, .T. ) ;
#11745=DIRECTION ( 'NONE',  ( 0.000000000000000000, 0.000000000000000000, 1.000000000000000000 ) ) ;
#11758=FILL_AREA_STYLE_COLOUR ( '', #21598 ) ;
#11776=VERTEX_POINT ( 'NONE', #21162 ) ;
#11803=ORIENTED_EDGE ( 'NONE', *, *, #6524, .F. ) ;
#11814=DIRECTION ( 'NONE',  ( 0.000000000000000000, 0.000000000000000000, -1.000000000000000000 ) ) ;
#11817=CARTESIAN_POINT ( 'NONE',  ( -29.69597781366221412, 27.99124249474150972, 70.25000000000000000 ) ) ;
#11819=ORIENTED_EDGE ( 'NONE', *, *, #13496, .T. ) ;
#11830=CIRCLE ( 'NONE', #15422, 0.2500000000000002220 ) ;
#11925=ORIENTED_EDGE ( 'NONE', *, *, #14319, .T. ) ;
#11928=CARTESIAN_POINT ( 'NONE',  ( -9.178906393579156386, 42.46645089659917716, 68.50000000000000000 ) ) ;
#11946=EDGE_CURVE ( 'NONE', #18991, #20665, #6839, .T. ) ;
#11947=EDGE_CURVE ( 'NONE', #16130, #7436, #17086, .T. ) ;
#11949=TOROIDAL_SURFACE ( 'NONE', #16953, 5.193574995607837863, 1.000000000000000000 ) ;
#11970=EDGE_CURVE ( 'NONE', #5130, #12408, #3139, .T. ) ;
#12010=CARTESIAN_POINT ( 'NONE',  ( -9.178906393579156386, 42.46645089659917716, 69.50000000000000000 ) ) ;
#12038=DIRECTION ( 'NONE',  ( 1.000000000000000000, 0.000000000000000000, 0.000000000000000000 ) ) ;
#12051=CARTESIAN_POINT ( 'NONE',  ( -29.69597781366221767, 56.94165929845684815, 70.50000000000000000 ) ) ;
#12070=EDGE_CURVE ( 'NONE', #897, #6536, #3239, .T. ) ;
#12091=ORIENTED_EDGE ( 'NONE', *, *, #13496, .F. ) ;
#12115=DIRECTION ( 'NONE',  ( 1.000000000000000000, 0.000000000000000000, 0.000000000000000000 ) ) ;
#12122=ADVANCED_FACE ( 'NONE', ( #3684 ), #18881, .T. ) ;
#12131=ORIENTED_EDGE ( 'NONE', *, *, #1589, .T. ) ;
#12134=CARTESIAN_POINT ( 'NONE',  ( 9.178906393579156386, 42.46645089659917716, 69.50000000000000000 ) ) ;
#12178=ORIENTED_EDGE ( 'NONE', *, *, #3556, .T. ) ;
#12194=CARTESIAN_POINT ( 'NONE',  ( 9.178906393579156386, 42.46645089659917716, 69.50000000000000000 ) ) ;
#12215=EDGE_CURVE ( 'NONE', #12408, #7436, #7370, .T. ) ;
#12226=DIRECTION ( 'NONE',  ( -1.000000000000000000, 0.000000000000000000, 0.000000000000000000 ) ) ;
#12240=EDGE_CURVE ( 'NONE', #11281, #17419, #4558, .T. ) ;
#12251=DIRECTION ( 'NONE',  ( -0.000000000000000000, 0.000000000000000000, 1.000000000000000000 ) ) ;
#12263=ADVANCED_FACE ( 'NONE', ( #9472 ), #13035, .F. ) ;
#12266=CIRCLE ( 'NONE', #2634, 0.2500000000000002220 ) ;
#12267=ORIENTED_EDGE ( 'NONE', *, *, #27, .T. ) ;
#12279=PLANE ( 'NONE',  #6544 ) ;
#12282=PLANE ( 'NONE',  #20994 ) ;
#12331=DIRECTION ( 'NONE',  ( 0.000000000000000000, 0.000000000000000000, -1.000000000000000000 ) ) ;
#12347=CARTESIAN_POINT ( 'NONE',  ( 29.69597781366221767, 26.24124249474150972, 68.75000000000000000 ) ) ;
#12369=ADVANCED_FACE ( 'NONE', ( #9881 ), #14226, .T. ) ;
#12384=DIRECTION ( 'NONE',  ( -0.000000000000000000, 0.000000000000000000, 1.000000000000000000 ) ) ;
#12394=FACE_OUTER_BOUND ( 'NONE', #19584, .T. ) ;
#12408=VERTEX_POINT ( 'NONE', #13668 ) ;
#12466=EDGE_CURVE ( 'NONE', #5063, #17549, #4839, .T. ) ;
#12467=EDGE_LOOP ( 'NONE', ( #6949, #14434, #8667, #12178 ) ) ;
#12475=CARTESIAN_POINT ( 'NONE',  ( -29.69597781366221767, 56.94165929845684815, 68.75000000000000000 ) ) ;
#12510=CIRCLE ( 'NONE', #4665, 0.2500000000000002220 ) ;
#12621=DIRECTION ( 'NONE',  ( 1.000000000000000000, 0.000000000000000000, 0.000000000000000000 ) ) ;
#12664=AXIS2_PLACEMENT_3D ( 'NONE', #8271, #1648, #21926 ) ;
#12750=AXIS2_PLACEMENT_3D ( 'NONE', #18254, #9656, #2823 ) ;
#12760=EDGE_LOOP ( 'NONE', ( #7982, #6569, #5010, #13435 ) ) ;
#12763=VECTOR ( 'NONE', #19670, 1000.000000000000000 ) ;
#12784=AXIS2_PLACEMENT_3D ( 'NONE', #12475, #12251, #6934 ) ;
#12820=ORIENTED_EDGE ( 'NONE', *, *, #1016, .T. ) ;
#12824=EDGE_LOOP ( 'NONE', ( #10779, #18969, #17972, #3903 ) ) ;
#12857=CARTESIAN_POINT ( 'NONE',  ( 4.985331397971318523, 42.46645089659917716, 69.50000000000000000 ) ) ;
#12893=CIRCLE ( 'NONE', #2141, 0.2500000000000002220 ) ;
#12897=ORIENTED_EDGE ( 'NONE', *, *, #4048, .T. ) ;
#12908=ORIENTED_EDGE ( 'NONE', *, *, #1173, .T. ) ;
#12948=DIRECTION ( 'NONE',  ( -1.000000000000000000, 0.000000000000000000, 0.000000000000000000 ) ) ;
#12950=DIRECTION ( 'NONE',  ( 1.000000000000000000, 0.000000000000000000, 0.000000000000000000 ) ) ;
#12962=DIRECTION ( 'NONE',  ( 1.224646799147353207E-16, 1.000000000000000000, 0.000000000000000000 ) ) ;
#12975=DIRECTION ( 'NONE',  ( 0.000000000000000000, -0.000000000000000000, -1.000000000000000000 ) ) ;
#12980=FILL_AREA_STYLE ('',( #11758 ) ) ;
#13008=DIRECTION ( 'NONE',  ( 1.000000000000000000, 0.000000000000000000, 0.000000000000000000 ) ) ;
#13024=DIRECTION ( 'NONE',  ( 1.000000000000000000, 0.000000000000000000, 0.000000000000000000 ) ) ;
#13027=ORIENTED_EDGE ( 'NONE', *, *, #14543, .T. ) ;
#13035=PLANE ( 'NONE',  #988 ) ;
#13038=ADVANCED_FACE ( 'NONE', ( #1169 ), #6236, .F. ) ;
#13048=CARTESIAN_POINT ( 'NONE',  ( -31.69597781366222122, 58.69165929845684815, 68.75000000000000000 ) ) ;
#13056=EDGE_CURVE ( 'NONE', #14159, #4394, #11160, .T. ) ;
#13068=ADVANCED_FACE ( 'NONE', ( #2748 ), #7917, .F. ) ;
#13081=DIRECTION ( 'NONE',  ( 0.000000000000000000, 0.000000000000000000, -1.000000000000000000 ) ) ;
#13084=CARTESIAN_POINT ( 'NONE',  ( 9.178906393579156386, 42.46645089659917716, 70.50000000000000000 ) ) ;
#13093=ORIENTED_EDGE ( 'NONE', *, *, #13103, .T. ) ;
#13096=CARTESIAN_POINT ( 'NONE',  ( -29.69597781366221767, 58.69165929845684104, 70.50000000000000000 ) ) ;
#13099=EDGE_LOOP ( 'NONE', ( #6106, #19304, #2651, #21085 ) ) ;
#13103=EDGE_CURVE ( 'NONE', #17419, #847, #14937, .T. ) ;
#13165=ORIENTED_EDGE ( 'NONE', *, *, #19216, .T. ) ;
#13167=AXIS2_PLACEMENT_3D ( 'NONE', #13048, #14745, #11390 ) ;
#13233=LINE ( 'NONE', #16363, #10016 ) ;
#13249=DIRECTION ( 'NONE',  ( 0.000000000000000000, -1.000000000000000000, 0.000000000000000000 ) ) ;
#13277=CYLINDRICAL_SURFACE ( 'NONE', #5776, 0.2500000000000002220 ) ;
#13288=CIRCLE ( 'NONE', #4725, 2.000000000000001776 ) ;
#13292=FACE_OUTER_BOUND ( 'NONE', #17416, .T. ) ;
#13306=ORIENTED_EDGE ( 'NONE', *, *, #17785, .T. ) ;
#13335=DIRECTION ( 'NONE',  ( 0.000000000000000000, 1.000000000000000000, -0.000000000000000000 ) ) ;
#13345=CARTESIAN_POINT ( 'NONE',  ( 9.178906393579156386, 42.46645089659917716, 70.50000000000000000 ) ) ;
#13386=FACE_OUTER_BOUND ( 'NONE', #14256, .T. ) ;
#13394=DIRECTION ( 'NONE',  ( 1.000000000000000000, 0.000000000000000000, 0.000000000000000000 ) ) ;
#13402=DIRECTION ( 'NONE',  ( 1.000000000000000000, 0.000000000000000000, 0.000000000000000000 ) ) ;
#13424=CARTESIAN_POINT ( 'NONE',  ( 3.985331397971318079, 42.46645089659917716, 70.50000000000000000 ) ) ;
#13435=ORIENTED_EDGE ( 'NONE', *, *, #4048, .F. ) ;
#13438=ADVANCED_FACE ( 'NONE', ( #21542 ), #19736, .T. ) ;
#13439=ORIENTED_EDGE ( 'NONE', *, *, #21708, .F. ) ;
#13470=CARTESIAN_POINT ( 'NONE',  ( -29.69597781366221767, 56.94165929845684815, 70.25000000000000000 ) ) ;
#13496=EDGE_CURVE ( 'NONE', #8252, #1910, #5077, .T. ) ;
#13506=CARTESIAN_POINT ( 'NONE',  ( -31.44597781366222122, 56.94165929845684815, 70.50000000000000000 ) ) ;
#13509=ORIENTED_EDGE ( 'NONE', *, *, #12240, .T. ) ;
#13542=AXIS2_PLACEMENT_3D ( 'NONE', #8030, #18078, #2434 ) ;
#13553=CARTESIAN_POINT ( 'NONE',  ( 31.69597781366222122, 27.99124249474150972, 68.75000000000000000 ) ) ;
#13564=ORIENTED_EDGE ( 'NONE', *, *, #3317, .T. ) ;
#13577=DIRECTION ( 'NONE',  ( -0.000000000000000000, -0.000000000000000000, -1.000000000000000000 ) ) ;
#13601=DIRECTION ( 'NONE',  ( 0.000000000000000000, -0.000000000000000000, -1.000000000000000000 ) ) ;
#13625=ORIENTED_EDGE ( 'NONE', *, *, #1267, .F. ) ;
#13668=CARTESIAN_POINT ( 'NONE',  ( 13.37248138918699425, 42.46645089659917716, 69.50000000000000000 ) ) ;
#13714=DIRECTION ( 'NONE',  ( -0.000000000000000000, 0.000000000000000000, 1.000000000000000000 ) ) ;
#13718=DIRECTION ( 'NONE',  ( -1.000000000000000000, 0.000000000000000000, -0.000000000000000000 ) ) ;
#13782=ORIENTED_EDGE ( 'NONE', *, *, #8425, .F. ) ;
#13815=CIRCLE ( 'NONE', #7764, 4.193574995607837863 ) ;
#13821=CLOSED_SHELL ( 'NONE', ( #15509, #6668, #2174, #13038, #16519, #14067, #3963, #3062, #12263, #13068, #10361, #17164, #603, #13438, #5805, #20658, #7804, #12369, #5865, #5470, #6093, #20836, #20982, #902, #8654, #8419, #20631, #11705, #656, #1646, #3196, #3646, #12122, #14419 ) ) ;
#13846=AXIS2_PLACEMENT_3D ( 'NONE', #7241, #3659, #19199 ) ;
#13892=VECTOR ( 'NONE', #9103, 1000.000000000000000 ) ;
#13893=EDGE_CURVE ( 'NONE', #11579, #5463, #3655, .T. ) ;
#13903=DIRECTION ( 'NONE',  ( 0.000000000000000000, 0.000000000000000000, 1.000000000000000000 ) ) ;
#13956=ORIENTED_EDGE ( 'NONE', *, *, #1016, .F. ) ;
#13979=EDGE_CURVE ( 'NONE', #7925, #11776, #18577, .T. ) ;
#13980=VECTOR ( 'NONE', #5309, 1000.000000000000000 ) ;
#13990=CARTESIAN_POINT ( 'NONE',  ( 31.69597781366222122, 27.99124249474150972, 70.25000000000000000 ) ) ;
#13995=( LENGTH_UNIT ( ) NAMED_UNIT ( * ) SI_UNIT ( .MILLI., .METRE. ) );
#13997=CARTESIAN_POINT ( 'NONE',  ( -31.69597781366222122, 58.94165929845684815, 70.50000000000000000 ) ) ;
#14014=LINE ( 'NONE', #20860, #5630 ) ;
#14041=ORIENTED_EDGE ( 'NONE', *, *, #20434, .F. ) ;
#14067=ADVANCED_FACE ( 'NONE', ( #12394, #2229, #9060 ), #12279, .F. ) ;
#14089=ORIENTED_EDGE ( 'NONE', *, *, #20702, .F. ) ;
#14095=DIRECTION ( 'NONE',  ( -2.105859220307292343E-16, 1.000000000000000000, 0.000000000000000000 ) ) ;
#14117=CARTESIAN_POINT ( 'NONE',  ( -29.69597781366221767, 58.69165929845684104, 70.50000000000000000 ) ) ;
#14159=VERTEX_POINT ( 'NONE', #2784 ) ;
#14170=CARTESIAN_POINT ( 'NONE',  ( 13.37248138918699425, 42.46645089659917716, 70.50000000000000000 ) ) ;
#14190=DIRECTION ( 'NONE',  ( 1.000000000000000000, 0.000000000000000000, 0.000000000000000000 ) ) ;
#14198=ORIENTED_EDGE ( 'NONE', *, *, #21540, .F. ) ;
#14205=ORIENTED_EDGE ( 'NONE', *, *, #14344, .T. ) ;
#14226=TOROIDAL_SURFACE ( 'NONE', #18510, 5.193574995607837863, 1.000000000000000000 ) ;
#14232=AXIS2_PLACEMENT_3D ( 'NONE', #9486, #16294, #978 ) ;
#14251=VECTOR ( 'NONE', #766, 1000.000000000000000 ) ;
#14256=EDGE_LOOP ( 'NONE', ( #18407, #13782, #5027, #15741 ) ) ;
#14319=EDGE_CURVE ( 'NONE', #5463, #12408, #9326, .T. ) ;
#14344=EDGE_CURVE ( 'NONE', #5463, #11579, #11486, .T. ) ;
#14370=DIRECTION ( 'NONE',  ( 0.000000000000000000, 1.000000000000000000, 0.000000000000000000 ) ) ;
#14384=ORIENTED_EDGE ( 'NONE', *, *, #8365, .T. ) ;
#14419=ADVANCED_FACE ( 'NONE', ( #15488 ), #157, .T. ) ;
#14434=ORIENTED_EDGE ( 'NONE', *, *, #9863, .T. ) ;
#14444=CARTESIAN_POINT ( 'NONE',  ( 4.985331397971318523, 42.46645089659917716, 68.50000000000000000 ) ) ;
#14460=AXIS2_PLACEMENT_3D ( 'NONE', #14818, #11364, #13024 ) ;
#14472=LINE ( 'NONE', #943, #1835 ) ;
#14473=VECTOR ( 'NONE', #16481, 1000.000000000000000 ) ;
#14489=VECTOR ( 'NONE', #3119, 1000.000000000000000 ) ;
#14508=FACE_OUTER_BOUND ( 'NONE', #15513, .T. ) ;
#14533=CARTESIAN_POINT ( 'NONE',  ( -4.985331397971318523, 42.46645089659917716, 69.50000000000000000 ) ) ;
#14543=EDGE_CURVE ( 'NONE', #15631, #5063, #11830, .T. ) ;
#14561=ORIENTED_EDGE ( 'NONE', *, *, #2991, .T. ) ;
#14622=CARTESIAN_POINT ( 'NONE',  ( -31.44597781366222122, 58.94165929845684815, 68.75000000000000000 ) ) ;
#14695=ORIENTED_EDGE ( 'NONE', *, *, #2311, .T. ) ;
#14706=DIRECTION ( 'NONE',  ( 1.000000000000000000, 0.000000000000000000, 0.000000000000000000 ) ) ;
#14726=EDGE_LOOP ( 'NONE', ( #10901, #9683, #12091, #11481 ) ) ;
#14745=DIRECTION ( 'NONE',  ( -1.000000000000000000, 1.094601647044990554E-16, -0.000000000000000000 ) ) ;
#14762=ORIENTED_EDGE ( 'NONE', *, *, #8425, .T. ) ;
#14768=LINE ( 'NONE', #15905, #13892 ) ;
#14776=( GEOMETRIC_REPRESENTATION_CONTEXT ( 3 ) GLOBAL_UNCERTAINTY_ASSIGNED_CONTEXT ( ( #8734 ) ) GLOBAL_UNIT_ASSIGNED_CONTEXT ( ( #6199, #3041, #1234 ) ) REPRESENTATION_CONTEXT ( 'NONE', 'WORKASPACE' ) );
#14782=( LENGTH_UNIT ( ) NAMED_UNIT ( * ) SI_UNIT ( .MILLI., .METRE. ) );
#14786=EDGE_LOOP ( 'NONE', ( #11644, #3046, #2308, #5658 ) ) ;
#14816=DIRECTION ( 'NONE',  ( 0.000000000000000000, 0.000000000000000000, 1.000000000000000000 ) ) ;
#14818=CARTESIAN_POINT ( 'NONE',  ( -29.69597781366221412, 27.99124249474150972, 68.75000000000000000 ) ) ;
#14841=CARTESIAN_POINT ( 'NONE',  ( 14.37248138918699425, 42.46645089659917716, 70.50000000000000000 ) ) ;
#14848=DIRECTION ( 'NONE',  ( 0.000000000000000000, 0.000000000000000000, -1.000000000000000000 ) ) ;
#14866=DIRECTION ( 'NONE',  ( -1.000000000000000000, 0.000000000000000000, 0.000000000000000000 ) ) ;
#14911=AXIS2_PLACEMENT_3D ( 'NONE', #7057, #5148, #6848 ) ;
#14917=ORIENTED_EDGE ( 'NONE', *, *, #18276, .T. ) ;
#14937=LINE ( 'NONE', #9910, #16825 ) ;
#14975=CARTESIAN_POINT ( 'NONE',  ( 9.178906393579156386, 42.46645089659917716, 70.50000000000000000 ) ) ;
#15023=( GEOMETRIC_REPRESENTATION_CONTEXT ( 3 ) GLOBAL_UNCERTAINTY_ASSIGNED_CONTEXT ( ( #18258 ) ) GLOBAL_UNIT_ASSIGNED_CONTEXT ( ( #13995, #8977, #19051 ) ) REPRESENTATION_CONTEXT ( 'NONE', 'WORKASPACE' ) );
#15027=DIRECTION ( 'NONE',  ( 0.000000000000000000, 0.000000000000000000, 1.000000000000000000 ) ) ;
#15029=CARTESIAN_POINT ( 'NONE',  ( 9.178906393579156386, 42.46645089659917716, 69.50000000000000000 ) ) ;
#15053=PRODUCT_DEFINITION ( 'UNKNOWN', '', #11207, #204 ) ;
#15087=VERTEX_POINT ( 'NONE', #20592 ) ;
#15144=DIRECTION ( 'NONE',  ( 0.000000000000000000, 1.000000000000000000, 0.000000000000000000 ) ) ;
#15171=DIRECTION ( 'NONE',  ( -0.000000000000000000, 0.000000000000000000, -1.000000000000000000 ) ) ;
#15181=PRODUCT ( 'Front Plate', 'Front Plate', '', ( #17238 ) ) ;
#15185=CARTESIAN_POINT ( 'NONE',  ( -31.69597781366222122, 58.94165929845684815, 68.75000000000000000 ) ) ;
#15188=DIRECTION ( 'NONE',  ( -0.000000000000000000, -0.000000000000000000, 1.000000000000000000 ) ) ;
#15208=DIRECTION ( 'NONE',  ( 0.000000000000000000, -0.000000000000000000, 1.000000000000000000 ) ) ;
#15220=SHAPE_DEFINITION_REPRESENTATION ( #9830, #7461 ) ;
#15325=ORIENTED_EDGE ( 'NONE', *, *, #27, .F. ) ;
#15332=CARTESIAN_POINT ( 'NONE',  ( -29.69597781366221767, 56.94165929845684815, 68.50000000000000000 ) ) ;
#15369=ORIENTED_EDGE ( 'NONE', *, *, #16309, .F. ) ;
#15386=EDGE_LOOP ( 'NONE', ( #13027, #1324, #14917, #11803 ) ) ;
#15391=DIRECTION ( 'NONE',  ( 1.000000000000000000, -0.000000000000000000, 0.000000000000000000 ) ) ;
#15406=ORIENTED_EDGE ( 'NONE', *, *, #21287, .F. ) ;
#15416=CARTESIAN_POINT ( 'NONE',  ( 29.69597781366221767, 27.99124249474150972, 70.25000000000000000 ) ) ;
#15422=AXIS2_PLACEMENT_3D ( 'NONE', #11008, #480, #20979 ) ;
#15461=CARTESIAN_POINT ( 'NONE',  ( -9.178906393579156386, 42.46645089659917716, 69.50000000000000000 ) ) ;
#15464=CARTESIAN_POINT ( 'NONE',  ( -14.37248138918699425, 42.46645089659917716, 69.50000000000000000 ) ) ;
#15478=MECHANICAL_DESIGN_GEOMETRIC_PRESENTATION_REPRESENTATION('',(#9778),#14776);
#15488=FACE_OUTER_BOUND ( 'NONE', #15386, .T. ) ;
#15493=VERTEX_POINT ( 'NONE', #1765 ) ;
#15500=CARTESIAN_POINT ( 'NONE',  ( -31.44597781366220701, -6.622080232047910987E-15, 68.50000000000000000 ) ) ;
#15504=DIRECTION ( 'NONE',  ( 0.000000000000000000, 0.000000000000000000, -1.000000000000000000 ) ) ;
#15509=ADVANCED_FACE ( 'NONE', ( #6931 ), #4132, .T. ) ;
#15513=EDGE_LOOP ( 'NONE', ( #17614, #13625, #5135, #17282 ) ) ;
#15540=DIRECTION ( 'NONE',  ( 0.000000000000000000, 0.000000000000000000, 1.000000000000000000 ) ) ;
#15554=CYLINDRICAL_SURFACE ( 'NONE', #8622, 2.000000000000001776 ) ;
#15575=DIRECTION ( 'NONE',  ( -0.000000000000000000, 0.000000000000000000, 1.000000000000000000 ) ) ;
#15611=DIRECTION ( 'NONE',  ( 1.000000000000000000, 0.000000000000000000, 0.000000000000000000 ) ) ;
#15613=EDGE_LOOP ( 'NONE', ( #14205, #8879 ) ) ;
#15631=VERTEX_POINT ( 'NONE', #9030 ) ;
#15656=DIRECTION ( 'NONE',  ( -0.000000000000000000, 0.000000000000000000, 1.000000000000000000 ) ) ;
#15658=VERTEX_POINT ( 'NONE', #4764 ) ;
#15693=DIRECTION ( 'NONE',  ( -2.105859220307292343E-16, 1.000000000000000000, -0.000000000000000000 ) ) ;
#15710=EDGE_LOOP ( 'NONE', ( #13306, #2723, #11114, #13439 ) ) ;
#15725=CARTESIAN_POINT ( 'NONE',  ( 9.178906393579156386, 42.46645089659917716, 68.50000000000000000 ) ) ;
#15741=ORIENTED_EDGE ( 'NONE', *, *, #17869, .F. ) ;
#15792=ORIENTED_EDGE ( 'NONE', *, *, #5946, .F. ) ;
#15802=ORIENTED_EDGE ( 'NONE', *, *, #2170, .F. ) ;
#15853=AXIS2_PLACEMENT_3D ( 'NONE', #15332, #10310, #8193 ) ;
#15896=VECTOR ( 'NONE', #15391, 1000.000000000000000 ) ;
#15905=CARTESIAN_POINT ( 'NONE',  ( -29.69597781366221412, 25.99124249474150972, 70.25000000000000000 ) ) ;
#15907=DIRECTION ( 'NONE',  ( 1.000000000000000000, 0.000000000000000000, 0.000000000000000000 ) ) ;
#15976=EDGE_CURVE ( 'NONE', #4042, #5726, #8890, .T. ) ;
#16053=CARTESIAN_POINT ( 'NONE',  ( -31.69597781366222122, 56.94165929845684815, 68.75000000000000000 ) ) ;
#16055=VERTEX_POINT ( 'NONE', #911 ) ;
#16074=CIRCLE ( 'NONE', #9685, 2.000000000000001776 ) ;
#16093=ORIENTED_EDGE ( 'NONE', *, *, #10910, .T. ) ;
#16118=ORIENTED_EDGE ( 'NONE', *, *, #1093, .F. ) ;
#16130=VERTEX_POINT ( 'NONE', #14444 ) ;
#16131=LINE ( 'NONE', #14117, #2494 ) ;
#16167=CARTESIAN_POINT ( 'NONE',  ( -31.44597781366222122, 56.94165929845684815, 68.50000000000000000 ) ) ;
#16171=FACE_BOUND ( 'NONE', #16836, .T. ) ;
#16191=CARTESIAN_POINT ( 'NONE',  ( 31.69597781366222122, 27.99124249474150972, 70.25000000000000000 ) ) ;
#16226=DIRECTION ( 'NONE',  ( 1.000000000000000000, 0.000000000000000000, 0.000000000000000000 ) ) ;
#16254=CYLINDRICAL_SURFACE ( 'NONE', #10615, 2.000000000000001776 ) ;
#16276=AXIS2_PLACEMENT_3D ( 'NONE', #19759, #1062, #2740 ) ;
#16285=EDGE_LOOP ( 'NONE', ( #4826, #3038, #4519, #5760 ) ) ;
#16286=DIRECTION ( 'NONE',  ( 2.105859220307292343E-16, -1.000000000000000000, 0.000000000000000000 ) ) ;
#16294=DIRECTION ( 'NONE',  ( 0.000000000000000000, -0.000000000000000000, -1.000000000000000000 ) ) ;
#16309=EDGE_CURVE ( 'NONE', #857, #7850, #7402, .T. ) ;
#16310=CIRCLE ( 'NONE', #18460, 0.2500000000000002220 ) ;
#16314=AXIS2_PLACEMENT_3D ( 'NONE', #15416, #10058, #13394 ) ;
#16323=DIRECTION ( 'NONE',  ( -0.000000000000000000, 0.000000000000000000, 1.000000000000000000 ) ) ;
#16339=ORIENTED_EDGE ( 'NONE', *, *, #16843, .T. ) ;
#16363=CARTESIAN_POINT ( 'NONE',  ( 4.985331397971318523, 42.46645089659917716, 70.50000000000000000 ) ) ;
#16392=DIRECTION ( 'NONE',  ( 0.000000000000000000, -0.000000000000000000, -1.000000000000000000 ) ) ;
#16415=ORIENTED_EDGE ( 'NONE', *, *, #21370, .F. ) ;
#16421=AXIS2_PLACEMENT_3D ( 'NONE', #20539, #2052, #12226 ) ;
#16426=AXIS2_PLACEMENT_3D ( 'NONE', #11817, #10273, #8366 ) ;
#16427=VECTOR ( 'NONE', #6427, 1000.000000000000000 ) ;
#16469=ORIENTED_EDGE ( 'NONE', *, *, #21145, .F. ) ;
#16481=DIRECTION ( 'NONE',  ( 0.000000000000000000, 1.000000000000000000, -0.000000000000000000 ) ) ;
#16504=DIRECTION ( 'NONE',  ( 1.000000000000000000, -0.000000000000000000, 0.000000000000000000 ) ) ;
#16517=CARTESIAN_POINT ( 'NONE',  ( -31.69597781366222122, 58.94165929845684815, 70.50000000000000000 ) ) ;
#16518=ORIENTED_EDGE ( 'NONE', *, *, #21271, .T. ) ;
#16519=ADVANCED_FACE ( 'NONE', ( #2433, #8636, #16171 ), #12282, .T. ) ;
#16550=FACE_OUTER_BOUND ( 'NONE', #13099, .T. ) ;
#16564=PRESENTATION_STYLE_ASSIGNMENT (( #11534 ) ) ;
#16611=ORIENTED_EDGE ( 'NONE', *, *, #21088, .F. ) ;
#16667=AXIS2_PLACEMENT_3D ( 'NONE', #4301, #5993, #11627 ) ;
#16680=CARTESIAN_POINT ( 'NONE',  ( -31.69597781366222122, 58.94165929845684815, 68.75000000000000000 ) ) ;
#16699=AXIS2_PLACEMENT_3D ( 'NONE', #21146, #12384, #4347 ) ;
#16727=DIRECTION ( 'NONE',  ( 0.000000000000000000, 0.000000000000000000, -1.000000000000000000 ) ) ;
#16730=AXIS2_PLACEMENT_3D ( 'NONE', #1903, #8745, #15540 ) ;
#16789=VERTEX_POINT ( 'NONE', #164 ) ;
#16805=AXIS2_PLACEMENT_3D ( 'NONE', #6185, #9412, #13081 ) ;
#16809=DIRECTION ( 'NONE',  ( -1.000000000000000000, 0.000000000000000000, 0.000000000000000000 ) ) ;
#16825=VECTOR ( 'NONE', #16727, 1000.000000000000000 ) ;
#16836=EDGE_LOOP ( 'NONE', ( #10192, #17135 ) ) ;
#16843=EDGE_CURVE ( 'NONE', #12408, #5130, #13815, .T. ) ;
#16861=CIRCLE ( 'NONE', #5804, 0.2500000000000002220 ) ;
#16927=CYLINDRICAL_SURFACE ( 'NONE', #6376, 4.193574995607837863 ) ;
#16933=ORIENTED_EDGE ( 'NONE', *, *, #5639, .F. ) ;
#16944=ORIENTED_EDGE ( 'NONE', *, *, #14319, .F. ) ;
#16953=AXIS2_PLACEMENT_3D ( 'NONE', #15029, #11655, #1484 ) ;
#17010=AXIS2_PLACEMENT_3D ( 'NONE', #15725, #17955, #395 ) ;
#17025=DIRECTION ( 'NONE',  ( 1.000000000000000000, 0.000000000000000000, 0.000000000000000000 ) ) ;
#17068=DIRECTION ( 'NONE',  ( 0.000000000000000000, -1.000000000000000000, 0.000000000000000000 ) ) ;
#17086=CIRCLE ( 'NONE', #8862, 4.193574995607837863 ) ;
#17117=ORIENTED_EDGE ( 'NONE', *, *, #3317, .F. ) ;
#17135=ORIENTED_EDGE ( 'NONE', *, *, #1363, .T. ) ;
#17164=ADVANCED_FACE ( 'NONE', ( #11661 ), #16927, .F. ) ;
#17207=CARTESIAN_POINT ( 'NONE',  ( 31.44597781366222122, 0.000000000000000000, 68.50000000000000000 ) ) ;
#17209=CARTESIAN_POINT ( 'NONE',  ( 31.69597781366222122, 58.94165929845684104, 70.50000000000000000 ) ) ;
#17238=PRODUCT_CONTEXT ( 'NONE', #1985, 'mechanical' ) ;
#17242=ORIENTED_EDGE ( 'NONE', *, *, #15976, .F. ) ;
#17276=ORIENTED_EDGE ( 'NONE', *, *, #1267, .T. ) ;
#17282=ORIENTED_EDGE ( 'NONE', *, *, #22146, .F. ) ;
#17325=LINE ( 'NONE', #16191, #14251 ) ;
#17327=CIRCLE ( 'NONE', #534, 0.2500000000000002220 ) ;
#17385=DIRECTION ( 'NONE',  ( 0.000000000000000000, -1.000000000000000000, 0.000000000000000000 ) ) ;
#17389=AXIS2_PLACEMENT_3D ( 'NONE', #9745, #12962, #14866 ) ;
#17416=EDGE_LOOP ( 'NONE', ( #20155, #7495, #15406, #8025 ) ) ;
#17419=VERTEX_POINT ( 'NONE', #21746 ) ;
#17429=VECTOR ( 'NONE', #4019, 1000.000000000000000 ) ;
#17489=AXIS2_PLACEMENT_3D ( 'NONE', #12010, #9006, #15907 ) ;
#17493=AXIS2_PLACEMENT_3D ( 'NONE', #9767, #1237, #16226 ) ;
#17520=VERTEX_POINT ( 'NONE', #13096 ) ;
#17541=ORIENTED_EDGE ( 'NONE', *, *, #10782, .T. ) ;
#17549=VERTEX_POINT ( 'NONE', #13553 ) ;
#17583=FACE_OUTER_BOUND ( 'NONE', #21056, .T. ) ;
#17614=ORIENTED_EDGE ( 'NONE', *, *, #1895, .T. ) ;
#17628=ORIENTED_EDGE ( 'NONE', *, *, #8365, .F. ) ;
#17671=CARTESIAN_POINT ( 'NONE',  ( 29.69597781366221767, 56.94165929845684104, 68.75000000000000000 ) ) ;
#17679=CARTESIAN_POINT ( 'NONE',  ( 29.69597781366221767, 25.99124249474150972, 70.25000000000000000 ) ) ;
#17769=CARTESIAN_POINT ( 'NONE',  ( 29.69597781366221767, 26.24124249474150972, 70.50000000000000000 ) ) ;
#17772=FACE_OUTER_BOUND ( 'NONE', #8626, .T. ) ;
#17785=EDGE_CURVE ( 'NONE', #4042, #10367, #8539, .T. ) ;
#17824=ORIENTED_EDGE ( 'NONE', *, *, #12215, .F. ) ;
#17855=FACE_OUTER_BOUND ( 'NONE', #4110, .T. ) ;
#17859=AXIS2_PLACEMENT_3D ( 'NONE', #11928, #20019, #4686 ) ;
#17864=CARTESIAN_POINT ( 'NONE',  ( 0.000000000000000000, 0.000000000000000000, 70.50000000000000000 ) ) ;
#17869=EDGE_CURVE ( 'NONE', #18991, #17549, #7108, .T. ) ;
#17874=AXIS2_PLACEMENT_3D ( 'NONE', #10976, #14095, #5633 ) ;
#17880=CARTESIAN_POINT ( 'NONE',  ( 31.69597781366222122, 56.94165929845684104, 70.25000000000000000 ) ) ;
#17936=CARTESIAN_POINT ( 'NONE',  ( -31.44597781366221412, 27.99124249474150972, 70.50000000000000000 ) ) ;
#17948=CARTESIAN_POINT ( 'NONE',  ( 31.44597781366222122, 27.99124249474150972, 68.75000000000000000 ) ) ;
#17955=DIRECTION ( 'NONE',  ( 0.000000000000000000, 0.000000000000000000, 1.000000000000000000 ) ) ;
#17965=CARTESIAN_POINT ( 'NONE',  ( -31.69597781366221412, 25.99124249474150972, 70.50000000000000000 ) ) ;
#17972=ORIENTED_EDGE ( 'NONE', *, *, #18276, .F. ) ;
#18000=CIRCLE ( 'NONE', #15853, 1.750000000000001554 ) ;
#18056=TOROIDAL_SURFACE ( 'NONE', #6302, 5.193574995607837863, 1.000000000000000000 ) ;
#18078=DIRECTION ( 'NONE',  ( -0.000000000000000000, 0.000000000000000000, 1.000000000000000000 ) ) ;
#18128=CYLINDRICAL_SURFACE ( 'NONE', #18995, 0.2500000000000002220 ) ;
#18129=EDGE_CURVE ( 'NONE', #11579, #5130, #8480, .T. ) ;
#18177=EDGE_LOOP ( 'NONE', ( #14384, #10247, #18562, #9506 ) ) ;
#18254=CARTESIAN_POINT ( 'NONE',  ( -9.178906393579156386, 42.46645089659917716, 70.50000000000000000 ) ) ;
#18258=UNCERTAINTY_MEASURE_WITH_UNIT (LENGTH_MEASURE( 1.000000000000000082E-05 ), #13995, 'distance_accuracy_value', 'NONE');
#18276=EDGE_CURVE ( 'NONE', #5726, #15087, #9933, .T. ) ;
#18290=CARTESIAN_POINT ( 'NONE',  ( -9.178906393579156386, 42.46645089659917716, 68.50000000000000000 ) ) ;
#18322=CARTESIAN_POINT ( 'NONE',  ( -29.69597781366221412, 26.24124249474150972, 68.50000000000000000 ) ) ;
#18407=ORIENTED_EDGE ( 'NONE', *, *, #21287, .T. ) ;
#18460=AXIS2_PLACEMENT_3D ( 'NONE', #18620, #15144, #13903 ) ;
#18496=AXIS2_PLACEMENT_3D ( 'NONE', #4800, #5257, #13402 ) ;
#18510=AXIS2_PLACEMENT_3D ( 'NONE', #15461, #1366, #17025 ) ;
#18552=CYLINDRICAL_SURFACE ( 'NONE', #12664, 0.2500000000000002220 ) ;
#18562=ORIENTED_EDGE ( 'NONE', *, *, #21419, .F. ) ;
#18567=EDGE_LOOP ( 'NONE', ( #14561, #2094, #16118, #19106 ) ) ;
#18577=LINE ( 'NONE', #3028, #18660 ) ;
#18589=SHAPE_REPRESENTATION_RELATIONSHIP ( 'NONE' , 'NONE' ,  #7461, #20354 ) ;
#18599=STYLED_ITEM ( 'NONE', ( #10538 ), #20594 ) ;
#18620=CARTESIAN_POINT ( 'NONE',  ( -31.44597781366221412, 27.99124249474150972, 68.75000000000000000 ) ) ;
#18655=FACE_OUTER_BOUND ( 'NONE', #15710, .T. ) ;
#18660=VECTOR ( 'NONE', #15208, 1000.000000000000000 ) ;
#18668=EDGE_CURVE ( 'NONE', #5841, #20665, #1354, .T. ) ;
#18682=AXIS2_PLACEMENT_3D ( 'NONE', #13997, #19153, #3837 ) ;
#18713=CARTESIAN_POINT ( 'NONE',  ( -31.69597781366222122, 56.94165929845684815, 70.50000000000000000 ) ) ;
#18753=DIRECTION ( 'NONE',  ( -0.000000000000000000, 0.000000000000000000, 1.000000000000000000 ) ) ;
#18771=FACE_OUTER_BOUND ( 'NONE', #14786, .T. ) ;
#18776=CARTESIAN_POINT ( 'NONE',  ( -0.000000000000000000, 26.24124249474150972, 68.50000000000000000 ) ) ;
#18881=TOROIDAL_SURFACE ( 'NONE', #5666, 1.750000000000000000, 0.2500000000000000000 ) ;
#18894=CARTESIAN_POINT ( 'NONE',  ( 0.000000000000000000, 26.24124249474150972, 70.25000000000000000 ) ) ;
#18902=DIRECTION ( 'NONE',  ( -0.000000000000000000, 0.000000000000000000, 1.000000000000000000 ) ) ;
#18911=CARTESIAN_POINT ( 'NONE',  ( -13.37248138918699425, 42.46645089659917716, 69.50000000000000000 ) ) ;
#18936=DIRECTION ( 'NONE',  ( 0.000000000000000000, -0.000000000000000000, -1.000000000000000000 ) ) ;
#18946=AXIS2_PLACEMENT_3D ( 'NONE', #1764, #20126, #9940 ) ;
#18958=ORIENTED_EDGE ( 'NONE', *, *, #18668, .T. ) ;
#18969=ORIENTED_EDGE ( 'NONE', *, *, #5140, .F. ) ;
#18991=VERTEX_POINT ( 'NONE', #1501 ) ;
#18995=AXIS2_PLACEMENT_3D ( 'NONE', #19818, #2814, #11745 ) ;
#19007=AXIS2_PLACEMENT_3D ( 'NONE', #19351, #21154, #5826 ) ;
#19051=( NAMED_UNIT ( * ) SI_UNIT ( $, .STERADIAN. ) SOLID_ANGLE_UNIT ( ) );
#19084=ORIENTED_EDGE ( 'NONE', *, *, #16843, .F. ) ;
#19094=CARTESIAN_POINT ( 'NONE',  ( -29.69597781366221767, 58.94165929845684815, 70.50000000000000000 ) ) ;
#19106=ORIENTED_EDGE ( 'NONE', *, *, #1138, .F. ) ;
#19135=DIRECTION ( 'NONE',  ( -0.000000000000000000, 0.000000000000000000, 1.000000000000000000 ) ) ;
#19143=CIRCLE ( 'NONE', #9848, 0.2500000000000002220 ) ;
#19153=DIRECTION ( 'NONE',  ( -1.094601647044990554E-16, -1.000000000000000000, 0.000000000000000000 ) ) ;
#19199=DIRECTION ( 'NONE',  ( -1.000000000000000000, 0.000000000000000000, 0.000000000000000000 ) ) ;
#19203=LINE ( 'NONE', #19094, #20785 ) ;
#19216=EDGE_CURVE ( 'NONE', #11776, #8252, #14014, .T. ) ;
#19272=FILL_AREA_STYLE_COLOUR ( '', #26 ) ;
#19304=ORIENTED_EDGE ( 'NONE', *, *, #10910, .F. ) ;
#19351=CARTESIAN_POINT ( 'NONE',  ( -9.178906393579156386, 42.46645089659917716, 70.50000000000000000 ) ) ;
#19390=AXIS2_PLACEMENT_3D ( 'NONE', #15464, #1704, #16809 ) ;
#19440=DIRECTION ( 'NONE',  ( 1.000000000000000000, 0.000000000000000000, 0.000000000000000000 ) ) ;
#19584=EDGE_LOOP ( 'NONE', ( #13564, #17276, #12908, #16093, #14762, #17541, #9981, #21784 ) ) ;
#19644=DIRECTION ( 'NONE',  ( 0.000000000000000000, 0.000000000000000000, 1.000000000000000000 ) ) ;
#19670=DIRECTION ( 'NONE',  ( 1.000000000000000000, -1.094601647044990554E-16, -0.000000000000000000 ) ) ;
#19704=DIRECTION ( 'NONE',  ( 1.000000000000000000, 0.000000000000000000, 0.000000000000000000 ) ) ;
#19736=CYLINDRICAL_SURFACE ( 'NONE', #1125, 2.000000000000001776 ) ;
#19750=AXIS2_PLACEMENT_3D ( 'NONE', #17965, #8016, #4541 ) ;
#19759=CARTESIAN_POINT ( 'NONE',  ( -29.69597781366221412, 26.24124249474150972, 68.75000000000000000 ) ) ;
#19791=CYLINDRICAL_SURFACE ( 'NONE', #13167, 0.2500000000000002220 ) ;
#19812=CARTESIAN_POINT ( 'NONE',  ( -4.985331397971318523, 42.46645089659917716, 68.50000000000000000 ) ) ;
#19818=CARTESIAN_POINT ( 'NONE',  ( 31.44597781366222122, 58.94165929845684104, 68.75000000000000000 ) ) ;
#19857=DIRECTION ( 'NONE',  ( -0.000000000000000000, -0.000000000000000000, -1.000000000000000000 ) ) ;
#19882=DIRECTION ( 'NONE',  ( 0.000000000000000000, 0.000000000000000000, -1.000000000000000000 ) ) ;
#19884=ORIENTED_EDGE ( 'NONE', *, *, #2170, .T. ) ;
#19914=AXIS2_PLACEMENT_3D ( 'NONE', #7868, #12975, #4487 ) ;
#19940=AXIS2_PLACEMENT_3D ( 'NONE', #2122, #15656, #7283 ) ;
#19978=AXIS2_PLACEMENT_3D ( 'NONE', #11176, #6173, #12621 ) ;
#20012=DIRECTION ( 'NONE',  ( -2.105859220307292343E-16, 1.000000000000000000, 0.000000000000000000 ) ) ;
#20019=DIRECTION ( 'NONE',  ( 0.000000000000000000, 0.000000000000000000, 1.000000000000000000 ) ) ;
#20075=DIRECTION ( 'NONE',  ( -0.000000000000000000, -0.000000000000000000, -1.000000000000000000 ) ) ;
#20097=FACE_OUTER_BOUND ( 'NONE', #6364, .T. ) ;
#20105=DIRECTION ( 'NONE',  ( -1.000000000000000000, 0.000000000000000000, 0.000000000000000000 ) ) ;
#20125=DIRECTION ( 'NONE',  ( -0.000000000000000000, 0.000000000000000000, 1.000000000000000000 ) ) ;
#20126=DIRECTION ( 'NONE',  ( -0.000000000000000000, 0.000000000000000000, 1.000000000000000000 ) ) ;
#20155=ORIENTED_EDGE ( 'NONE', *, *, #4879, .F. ) ;
#20259=DIRECTION ( 'NONE',  ( 0.000000000000000000, -0.000000000000000000, -1.000000000000000000 ) ) ;
#20316=EDGE_CURVE ( 'NONE', #16789, #17520, #16131, .T. ) ;
#20354=ADVANCED_BREP_SHAPE_REPRESENTATION ( '', ( #20594, #17493 ), #6222 ) ;
#20372=CIRCLE ( 'NONE', #16426, 2.000000000000001776 ) ;
#20434=EDGE_CURVE ( 'NONE', #5130, #16130, #13233, .T. ) ;
#20530=DIRECTION ( 'NONE',  ( 0.000000000000000000, 0.000000000000000000, 1.000000000000000000 ) ) ;
#20539=CARTESIAN_POINT ( 'NONE',  ( 9.178906393579156386, 42.46645089659917716, 70.50000000000000000 ) ) ;
#20579=CARTESIAN_POINT ( 'NONE',  ( 29.69597781366221767, 25.99124249474150972, 70.50000000000000000 ) ) ;
#20592=CARTESIAN_POINT ( 'NONE',  ( 31.44597781366222122, 56.94165929845684104, 70.50000000000000000 ) ) ;
#20594=MANIFOLD_SOLID_BREP ( 'Stock-MAS-696-1', #13821 ) ;
#20631=ADVANCED_FACE ( 'NONE', ( #2025 ), #20733, .T. ) ;
#20658=ADVANCED_FACE ( 'NONE', ( #17583 ), #15554, .T. ) ;
#20665=VERTEX_POINT ( 'NONE', #17679 ) ;
#20702=EDGE_CURVE ( 'NONE', #16055, #7987, #21128, .T. ) ;
#20729=CARTESIAN_POINT ( 'NONE',  ( -31.44597781366221412, 27.99124249474150972, 68.50000000000000000 ) ) ;
#20733=CYLINDRICAL_SURFACE ( 'NONE', #17874, 0.2500000000000002220 ) ;
#20778=AXIS2_PLACEMENT_3D ( 'NONE', #21675, #16504, #8131 ) ;
#20785=VECTOR ( 'NONE', #283, 1000.000000000000000 ) ;
#20836=ADVANCED_FACE ( 'NONE', ( #16550 ), #18128, .T. ) ;
#20837=CARTESIAN_POINT ( 'NONE',  ( 29.69597781366221767, 56.94165929845684104, 70.25000000000000000 ) ) ;
#20840=DIRECTION ( 'NONE',  ( 1.000000000000000000, 0.000000000000000000, 0.000000000000000000 ) ) ;
#20843=FILL_AREA_STYLE ('',( #19272 ) ) ;
#20851=ORIENTED_EDGE ( 'NONE', *, *, #13103, .F. ) ;
#20860=CARTESIAN_POINT ( 'NONE',  ( -31.69597781366222122, 56.94165929845684815, 70.25000000000000000 ) ) ;
#20863=DIRECTION ( 'NONE',  ( -1.000000000000000000, 1.094601647044990554E-16, -0.000000000000000000 ) ) ;
#20937=ORIENTED_EDGE ( 'NONE', *, *, #11946, .T. ) ;
#20979=DIRECTION ( 'NONE',  ( 0.000000000000000000, 0.000000000000000000, 1.000000000000000000 ) ) ;
#20982=ADVANCED_FACE ( 'NONE', ( #21479 ), #13277, .T. ) ;
#20992=EDGE_LOOP ( 'NONE', ( #5739, #9439 ) ) ;
#20994=AXIS2_PLACEMENT_3D ( 'NONE', #17864, #19135, #2542 ) ;
#21028=VECTOR ( 'NONE', #15188, 1000.000000000000000 ) ;
#21056=EDGE_LOOP ( 'NONE', ( #17242, #5941, #20851, #14695 ) ) ;
#21059=ORIENTED_EDGE ( 'NONE', *, *, #11970, .T. ) ;
#21085=ORIENTED_EDGE ( 'NONE', *, *, #9863, .F. ) ;
#21088=EDGE_CURVE ( 'NONE', #7987, #8010, #6038, .T. ) ;
#21111=ORIENTED_EDGE ( 'NONE', *, *, #4398, .F. ) ;
#21128=CIRCLE ( 'NONE', #16805, 1.000000000000000888 ) ;
#21145=EDGE_CURVE ( 'NONE', #7850, #7284, #6926, .T. ) ;
#21146=CARTESIAN_POINT ( 'NONE',  ( -29.69597781366221412, 27.99124249474150972, 68.75000000000000000 ) ) ;
#21154=DIRECTION ( 'NONE',  ( 0.000000000000000000, -0.000000000000000000, -1.000000000000000000 ) ) ;
#21162=CARTESIAN_POINT ( 'NONE',  ( -31.69597781366221412, 27.99124249474150972, 70.25000000000000000 ) ) ;
#21222=DIRECTION ( 'NONE',  ( 0.000000000000000000, 0.000000000000000000, 1.000000000000000000 ) ) ;
#21257=DIRECTION ( 'NONE',  ( 1.000000000000000000, 0.000000000000000000, -0.000000000000000000 ) ) ;
#21263=EDGE_LOOP ( 'NONE', ( #7997, #12820 ) ) ;
#21271=EDGE_CURVE ( 'NONE', #4394, #11281, #19203, .T. ) ;
#21287=EDGE_CURVE ( 'NONE', #18991, #1460, #7163, .T. ) ;
#21311=LINE ( 'NONE', #4297, #14473 ) ;
#21343=EDGE_CURVE ( 'NONE', #7284, #1910, #12893, .T. ) ;
#21359=DIRECTION ( 'NONE',  ( 1.000000000000000000, 0.000000000000000000, 0.000000000000000000 ) ) ;
#21370=EDGE_CURVE ( 'NONE', #4394, #1910, #11110, .T. ) ;
#21402=CYLINDRICAL_SURFACE ( 'NONE', #21613, 0.2500000000000002220 ) ;
#21419=EDGE_CURVE ( 'NONE', #5585, #8010, #6829, .T. ) ;
#21460=CARTESIAN_POINT ( 'NONE',  ( -9.178906393579156386, 42.46645089659917716, 70.50000000000000000 ) ) ;
#21479=FACE_OUTER_BOUND ( 'NONE', #2235, .T. ) ;
#21491=ORIENTED_EDGE ( 'NONE', *, *, #2990, .F. ) ;
#21492=CARTESIAN_POINT ( 'NONE',  ( -29.69597781366221767, 56.94165929845684815, 70.50000000000000000 ) ) ;
#21540=EDGE_CURVE ( 'NONE', #6536, #11776, #12510, .T. ) ;
#21542=FACE_OUTER_BOUND ( 'NONE', #3435, .T. ) ;
#21557=CARTESIAN_POINT ( 'NONE',  ( -13.37248138918699425, 42.46645089659917716, 70.50000000000000000 ) ) ;
#21575=DIRECTION ( 'NONE',  ( 1.000000000000000000, 0.000000000000000000, -0.000000000000000000 ) ) ;
#21598=COLOUR_RGB ( '', 0.09019608, 0.27058824, 0.51372549) ;
#21613=AXIS2_PLACEMENT_3D ( 'NONE', #7635, #5956, #7863 ) ;
#21656=LINE ( 'NONE', #6326, #10328 ) ;
#21675=CARTESIAN_POINT ( 'NONE',  ( -29.69597781366221767, 58.69165929845684815, 68.75000000000000000 ) ) ;
#21708=EDGE_CURVE ( 'NONE', #4042, #847, #16074, .T. ) ;
#21743=CARTESIAN_POINT ( 'NONE',  ( -29.69597781366221767, 58.94165929845684815, 68.75000000000000000 ) ) ;
#21746=CARTESIAN_POINT ( 'NONE',  ( 29.69597781366221767, 58.94165929845684104, 70.25000000000000000 ) ) ;
#21777=DIRECTION ( 'NONE',  ( -0.000000000000000000, 0.000000000000000000, 1.000000000000000000 ) ) ;
#21784=ORIENTED_EDGE ( 'NONE', *, *, #21145, .T. ) ;
#21926=DIRECTION ( 'NONE',  ( 0.000000000000000000, 0.000000000000000000, -1.000000000000000000 ) ) ;
#21954=EDGE_LOOP ( 'NONE', ( #13093, #9153, #16518, #13509 ) ) ;
#22031=CYLINDRICAL_SURFACE ( 'NONE', #5516, 0.2500000000000002220 ) ;
#22081=TOROIDAL_SURFACE ( 'NONE', #19940, 1.750000000000000000, 0.2500000000000000000 ) ;
#22146=EDGE_CURVE ( 'NONE', #847, #4394, #9871, .T. ) ;
ENDSEC;
END-ISO-10303-21;
